ISO-10303-21;
HEADER;
FILE_DESCRIPTION (('STEP AP214'),
    '1' );
FILE_NAME ('hex flange nut gradea_iso_ISO - 4161 - M5 - N.step',
    '2026-10-24T14:05:44',
    ( '' ),
    ( '' ),
    'SwSTEP 2.0',
    'SolidWorks 2026',
    '' );
FILE_SCHEMA (( 'AUTOMOTIVE_DESIGN' ));
ENDSEC;

DATA;
#5=DIRECTION ( 'NONE',  ( -0.000000000000000000, -0.000000000000000000, 1.000000000000000000 ) ) ;
#7=VERTEX_POINT ( 'NONE', #676 ) ;
#18=DIRECTION ( 'NONE',  ( -1.000000000000000000, 0.000000000000000000, 0.000000000000000000 ) ) ;
#19=CARTESIAN_POINT ( 'NONE',  ( -4.000000000000000000, -2.309401076758512694, -5.000000000000000000 ) ) ;
#34=ORIENTED_EDGE ( 'NONE', *, *, #6882, .F. ) ;
#36=EDGE_LOOP ( 'NONE', ( #2850, #5154, #2627, #2005, #1100 ) ) ;
#42=CARTESIAN_POINT ( 'NONE',  ( -4.000000000000000000, 2.309401076758498483, -0.4999999999999927280 ) ) ;
#55=ORIENTED_EDGE ( 'NONE', *, *, #575, .F. ) ;
#65=DIRECTION ( 'NONE',  ( 0.000000000000000000, 0.000000000000000000, 1.000000000000000000 ) ) ;
#68=CARTESIAN_POINT ( 'NONE',  ( -4.000000000000000000, -2.309401076758512694, -3.433295621305382461 ) ) ;
#71=ORIENTED_EDGE ( 'NONE', *, *, #6101, .T. ) ;
#73=AXIS2_PLACEMENT_3D ( 'NONE', #2890, #4175, #5910 ) ;
#75=AXIS2_PLACEMENT_3D ( 'NONE', #5132, #5651, #4005 ) ;
#76=VERTEX_POINT ( 'NONE', #5837 ) ;
#87=AXIS2_PLACEMENT_3D ( 'NONE', #968, #3225, #5526 ) ;
#93=DIRECTION ( 'NONE',  ( 0.000000000000000000, 0.000000000000000000, 1.000000000000000000 ) ) ;
#103=ORIENTED_EDGE ( 'NONE', *, *, #104, .F. ) ;
#104=EDGE_CURVE ( 'NONE', #3497, #7, #5877, .T. ) ;
#122=CARTESIAN_POINT ( 'NONE',  ( 0.6640947660595348800, -4.471078309994175548, -3.602146406945708090 ) ) ;
#123=FACE_OUTER_BOUND ( 'NONE', #3816, .T. ) ;
#125=CARTESIAN_POINT ( 'NONE',  ( -6.473970235329672780E-16, -4.862606272033106691, -3.745885042887442395 ) ) ;
#134=CARTESIAN_POINT ( 'NONE',  ( -3.349226789952655547, -2.685125164760744809, -0.2236248678334863682 ) ) ;
#136=EDGE_LOOP ( 'NONE', ( #7154, #5088, #1278, #4786 ) ) ;
#144=CARTESIAN_POINT ( 'NONE',  ( -3.333333333333332149, -2.694301256218264218, -3.300726591567082036 ) ) ;
#146=( BOUNDED_SURFACE ( )  B_SPLINE_SURFACE ( 3, 2, ( 
 ( #6466, #1910, #6397 ),
 ( #629, #5334, #5259 ),
 ( #1805, #4662, #5832 ),
 ( #1324, #4699, #1848 ),
 ( #734, #2886, #1879 ),
 ( #5298, #2440, #4772 ) ),
 .UNSPECIFIED., .F., .F., .F. ) 
 B_SPLINE_SURFACE_WITH_KNOTS ( ( 4, 2, 4 ),
 ( 3, 3 ),
 ( 0.02027752710269158445, 0.02273781595091097299, 0.02519810479913036153 ),
 ( 0.000000000000000000, 1.000000000000000000 ),
 .UNSPECIFIED. ) 
 GEOMETRIC_REPRESENTATION_ITEM ( )  RATIONAL_B_SPLINE_SURFACE ( (
 ( 1.000000000000000000, 0.8047781431712808242, 1.000000000000000000),
 ( 1.000000000000000000, 0.8123773247083928561, 1.000000000000000000),
 ( 1.000000000000000000, 0.8190670192154906326, 1.000000000000000000),
 ( 1.000000000000000000, 0.8192353552912178261, 1.000000000000000000),
 ( 1.000000000000000000, 0.8126132098226825917, 1.000000000000000000),
 ( 1.000000000000000000, 0.8047712465856394770, 1.000000000000000000) ) ) 
 REPRESENTATION_ITEM ( '' )  SURFACE ( )  );
#148=CARTESIAN_POINT ( 'NONE',  ( 4.000000000000000000, 2.309401076758497151, -5.000000000000000000 ) ) ;
#162=CARTESIAN_POINT ( 'NONE',  ( 0.000000000000000000, 0.000000000000000000, -5.000000000000000000 ) ) ;
#163=ORIENTED_EDGE ( 'NONE', *, *, #1002, .T. ) ;
#166=CARTESIAN_POINT ( 'NONE',  ( -3.455068668934486276, 2.624017327439035707, -3.316620875263955437 ) ) ;
#168=CARTESIAN_POINT ( 'NONE',  ( -0.3208286057739654917, 4.433571671609680465, -0.3503314178412548774 ) ) ;
#170=( GEOMETRIC_REPRESENTATION_CONTEXT ( 3 ) GLOBAL_UNCERTAINTY_ASSIGNED_CONTEXT ( ( #6164 ) ) GLOBAL_UNIT_ASSIGNED_CONTEXT ( ( #1926, #3047, #2969 ) ) REPRESENTATION_CONTEXT ( 'NONE', 'WORKASPACE' ) );
#182=CARTESIAN_POINT ( 'NONE',  ( -2.000000000000002665, -3.464101615137770374, -3.142992957459237680 ) ) ;
#184=EDGE_CURVE ( 'NONE', #3899, #7, #6874, .T. ) ;
#188=DIRECTION ( 'NONE',  ( 0.000000000000000000, 0.000000000000000000, 1.000000000000000000 ) ) ;
#192=ORIENTED_EDGE ( 'NONE', *, *, #3648, .F. ) ;
#200=DIRECTION ( 'NONE',  ( 1.000000000000000000, 0.000000000000000000, 0.000000000000000000 ) ) ;
#202=CIRCLE ( 'NONE', #2702, 2.499999999999999556 ) ;
#207=CARTESIAN_POINT ( 'NONE',  ( -0.5449313310646672903, -4.304185902836978883, -3.316620875263469159 ) ) ;
#208=CARTESIAN_POINT ( 'NONE',  ( -4.000000000000000000, 0.000000000000000000, 0.000000000000000000 ) ) ;
#213=PRODUCT_DEFINITION ( 'UNKNOWN', '', #6388, #5035 ) ;
#214=VERTEX_POINT ( 'NONE', #7299 ) ;
#220=ORIENTED_EDGE ( 'NONE', *, *, #7013, .F. ) ;
#259=ORIENTED_EDGE ( 'NONE', *, *, #7249, .T. ) ;
#273=CARTESIAN_POINT ( 'NONE',  ( -4.235886605889389145, -2.417314728048544303, -3.751161874094020909 ) ) ;
#296=AXIS2_PLACEMENT_3D ( 'NONE', #6685, #4909, #7197 ) ;
#297=CARTESIAN_POINT ( 'NONE',  ( -5.384454397937118664, 6.594054843588581554E-16, -4.484454397937119197 ) ) ;
#301=ADVANCED_FACE ( 'NONE', ( #5506 ), #2054, .T. ) ;
#308=DIRECTION ( 'NONE',  ( -0.000000000000000000, 0.000000000000000000, -1.000000000000000000 ) ) ;
#339=CARTESIAN_POINT ( 'NONE',  ( 4.000000000000000000, -0.8732470631449981147, -3.223155494240760088 ) ) ;
#351=CARTESIAN_POINT ( 'NONE',  ( 4.000000000000000888, 1.563622288139206118, -0.2253451193528334950 ) ) ;
#356=CARTESIAN_POINT ( 'NONE',  ( -6.259644161404862988E-16, -4.618802153517027165, -3.504271511726793076 ) ) ;
#362=DIRECTION ( 'NONE',  ( -1.000000000000000000, 0.000000000000000000, 0.000000000000000000 ) ) ;
#369=AXIS2_PLACEMENT_3D ( 'NONE', #1171, #3902, #2166 ) ;
#374=MECHANICAL_DESIGN_GEOMETRIC_PRESENTATION_REPRESENTATION('',(#6844),#3015);
#375=CARTESIAN_POINT ( 'NONE',  ( 4.211399257449709665, -2.459727064652517114, -3.751161691472417736 ) ) ;
#386=CARTESIAN_POINT ( 'NONE',  ( 4.235886605889389145, 2.417314728048528760, -3.751161874094018245 ) ) ;
#394=ORIENTED_EDGE ( 'NONE', *, *, #4580, .T. ) ;
#396=CIRCLE ( 'NONE', #2290, 0.5155456020628804703 ) ;
#399=CARTESIAN_POINT ( 'NONE',  ( 0.000000000000000000, 0.000000000000000000, 0.000000000000000000 ) ) ;
#410=CIRCLE ( 'NONE', #1470, 4.000000000000000000 ) ;
#412=AXIS2_PLACEMENT_3D ( 'NONE', #4911, #6123, #5072 ) ;
#417=ORIENTED_EDGE ( 'NONE', *, *, #4078, .F. ) ;
#428=DIRECTION ( 'NONE',  ( 0.5000000000000022204, 0.8660254037844374864, -0.000000000000000000 ) ) ;
#431=VERTEX_POINT ( 'NONE', #5361 ) ;
#436=CARTESIAN_POINT ( 'NONE',  ( -4.000000000000000000, 0.000000000000000000, 0.000000000000000000 ) ) ;
#439=AXIS2_PLACEMENT_3D ( 'NONE', #1753, #4533, #2236 ) ;
#442=VECTOR ( 'NONE', #1696, 1000.000000000000114 ) ;
#445=CARTESIAN_POINT ( 'NONE',  ( -1.828356344711647319, -3.563200125723192002, -1.076197711133951296E-14 ) ) ;
#461=B_SPLINE_CURVE_WITH_KNOTS ( 'NONE', 3,
 ( #1150, #4028, #622, #2880, #68 ),
 .UNSPECIFIED., .F., .F.,
 ( 4, 1, 4 ),
 ( 0.000000000000000000, 0.002309401076758505790, 0.004618802153517011580 ),
 .UNSPECIFIED. ) ;
#470=CARTESIAN_POINT ( 'NONE',  ( 0.000000000000000000, 0.000000000000000000, 0.000000000000000000 ) ) ;
#486=ORIENTED_EDGE ( 'NONE', *, *, #2822, .F. ) ;
#487=ADVANCED_FACE ( 'NONE', ( #5469 ), #2188, .T. ) ;
#493=ORIENTED_EDGE ( 'NONE', *, *, #3790, .T. ) ;
#498=EDGE_LOOP ( 'NONE', ( #4214, #3564, #961, #4905, #71 ) ) ;
#499=CARTESIAN_POINT ( 'NONE',  ( -4.197393957002303999, 0.4069871074557429025, -3.503767560748926257 ) ) ;
#502=ORIENTED_EDGE ( 'NONE', *, *, #7249, .F. ) ;
#504=CARTESIAN_POINT ( 'NONE',  ( 3.540020015735602765, 2.810662092924382627, -3.602146406945867962 ) ) ;
#511=EDGE_CURVE ( 'NONE', #4692, #7233, #922, .T. ) ;
#536=ADVANCED_FACE ( 'NONE', ( #4765 ), #3613, .T. ) ;
#549=CARTESIAN_POINT ( 'NONE',  ( 4.204015924366189871, -1.626724848190933548, -3.610627190413393084 ) ) ;
#555=CARTESIAN_POINT ( 'NONE',  ( 4.211140560182196957, -2.431303136016555122, -3.745885042887436622 ) ) ;
#557=CIRCLE ( 'NONE', #6773, 0.5155456020628804703 ) ;
#575=EDGE_CURVE ( 'NONE', #1949, #4530, #5787, .T. ) ;
#580=CARTESIAN_POINT ( 'NONE',  ( -4.197393957002303999, -7.773935952363655451E-14, -3.503767560748929810 ) ) ;
#599=ADVANCED_FACE ( 'NONE', ( #4872 ), #1488, .T. ) ;
#605=CARTESIAN_POINT ( 'NONE',  ( -4.207491450040567571, 2.029819825146470524, -3.671670828759566074 ) ) ;
#608=ADVANCED_FACE ( 'NONE', ( #5617 ), #1013, .T. ) ;
#614=CARTESIAN_POINT ( 'NONE',  ( 4.197393957002303999, 7.772902908466098641E-14, -3.503767560748929810 ) ) ;
#619=CARTESIAN_POINT ( 'NONE',  ( -4.000000000000000000, 2.309401076758498483, -5.000000000000000000 ) ) ;
#622=CARTESIAN_POINT ( 'NONE',  ( -4.000000000000000000, -7.806255641895631925E-15, -3.142992957459232350 ) ) ;
#623=EDGE_CURVE ( 'NONE', #1976, #3497, #2947, .T. ) ;
#624=ORIENTED_EDGE ( 'NONE', *, *, #6068, .T. ) ;
#628=DIRECTION ( 'NONE',  ( 0.000000000000000000, 0.000000000000000000, 1.000000000000000000 ) ) ;
#629=CARTESIAN_POINT ( 'NONE',  ( -4.000000000000000000, 1.700094919196744270, -3.320312364301766017 ) ) ;
#637=DIRECTION ( 'NONE',  ( -1.000000000000000000, 0.000000000000000000, 0.000000000000000000 ) ) ;
#663=ORIENTED_EDGE ( 'NONE', *, *, #1944, .F. ) ;
#676=CARTESIAN_POINT ( 'NONE',  ( -4.000000000000000000, 2.309401076758498483, -3.433295621305379353 ) ) ;
#686=( NAMED_UNIT ( * ) SI_UNIT ( $, .STERADIAN. ) SOLID_ANGLE_UNIT ( ) );
#688=DIRECTION ( 'NONE',  ( 1.000000000000000000, 0.000000000000000000, 0.000000000000000000 ) ) ;
#693=CARTESIAN_POINT ( 'NONE',  ( -2.000000000000006661, 3.464101615137750834, 0.000000000000000000 ) ) ;
#699=DIRECTION ( 'NONE',  ( -1.000000000000000000, 0.000000000000000000, 0.000000000000000000 ) ) ;
#705=CARTESIAN_POINT ( 'NONE',  ( -3.355112389629170799, 2.681727112203152963, -0.2256878752776689534 ) ) ;
#709=VERTEX_POINT ( 'NONE', #3935 ) ;
#711=FACE_OUTER_BOUND ( 'NONE', #4712, .T. ) ;
#716=CYLINDRICAL_SURFACE ( 'NONE', #2053, 2.100000000000000089 ) ;
#719=VERTEX_POINT ( 'NONE', #3399 ) ;
#722=CARTESIAN_POINT ( 'NONE',  ( -4.236525694536558362, 2.416953475386465211, -3.751298745799836354 ) ) ;
#727=EDGE_CURVE ( 'NONE', #2273, #3217, #1357, .T. ) ;
#734=CARTESIAN_POINT ( 'NONE',  ( -4.000000000000000000, -1.680117682357936904, -3.316611593218794951 ) ) ;
#749=ORIENTED_EDGE ( 'NONE', *, *, #6006, .T. ) ;
#752=CARTESIAN_POINT ( 'NONE',  ( -1.287237434361707233, -3.875615274277397937, -3.430618716626816500 ) ) ;
#754=CARTESIAN_POINT ( 'NONE',  ( -0.6507732100473471171, 4.243078065514775510, -0.2236248678334823436 ) ) ;
#760=DIRECTION ( 'NONE',  ( 1.000000000000000000, 0.000000000000000000, 0.000000000000000000 ) ) ;
#766=CARTESIAN_POINT ( 'NONE',  ( 3.861362476283255685, 2.629030857715988656, -3.671615880910370500 ) ) ;
#784=CARTESIAN_POINT ( 'NONE',  ( 0.000000000000000000, 0.000000000000000000, -4.974599999999998801 ) ) ;
#789=AXIS2_PLACEMENT_3D ( 'NONE', #2244, #6905, #6338 ) ;
#792=B_SPLINE_CURVE_WITH_KNOTS ( 'NONE', 3,
 ( #3200, #6640, #861, #4950, #5387, #5546 ),
 .UNSPECIFIED., .F., .F.,
 ( 4, 2, 4 ),
 ( 0.003358874760055551890, 0.004541967308452098118, 0.005725059856848645212 ),
 .UNSPECIFIED. ) ;
#798=EDGE_LOOP ( 'NONE', ( #259, #1754, #103, #7151, #5288 ) ) ;
#804=CARTESIAN_POINT ( 'NONE',  ( -3.264650091097280831E-13, -4.796980096169642493, -3.721999068284424617 ) ) ;
#807=VERTEX_POINT ( 'NONE', #5838 ) ;
#810=ORIENTED_EDGE ( 'NONE', *, *, #3072, .F. ) ;
#829=CARTESIAN_POINT ( 'NONE',  ( -3.540020015735593439, -2.810662092924100630, -3.602146406945814672 ) ) ;
#831=CARTESIAN_POINT ( 'NONE',  ( 0.000000000000000000, 0.000000000000000000, -0.2800830152838844622 ) ) ;
#843=CARTESIAN_POINT ( 'NONE',  ( -4.000000000000000888, -2.309401076758512694, -3.504269196027526512 ) ) ;
#848=CARTESIAN_POINT ( 'NONE',  ( 4.000000000000000000, 0.8378280264232961239, -3.220590601395640018 ) ) ;
#851=DIRECTION ( 'NONE',  ( 0.000000000000000000, 0.000000000000000000, -1.000000000000000000 ) ) ;
#853=VERTEX_POINT ( 'NONE', #4710 ) ;
#861=CARTESIAN_POINT ( 'NONE',  ( 4.000000000000000000, -1.560351142792952617, -0.2242961665059816367 ) ) ;
#864=CARTESIAN_POINT ( 'NONE',  ( -4.000000000000000000, 0.3987449864459974846, -0.01220643443059782861 ) ) ;
#868=DIRECTION ( 'NONE',  ( 0.000000000000000000, 0.000000000000000000, -1.000000000000000000 ) ) ;
#872=VECTOR ( 'NONE', #2495, 999.9999999999998863 ) ;
#904=EDGE_LOOP ( 'NONE', ( #3846, #3143, #3187, #4503 ) ) ;
#922=B_SPLINE_CURVE_WITH_KNOTS ( 'NONE', 3,
 ( #3169, #356, #3590, #2467, #804, #3058 ),
 .UNSPECIFIED., .F., .F.,
 ( 4, 2, 4 ),
 ( 0.000000000000000000, 0.0002095117440854740156, 0.0004190234881709480313 ),
 .UNSPECIFIED. ) ;
#930=CARTESIAN_POINT ( 'NONE',  ( -4.154094228333456762, 2.398367420968013253, -3.721909803043220055 ) ) ;
#946=CARTESIAN_POINT ( 'NONE',  ( 2.171643655288379993, -3.365003104552334978, -1.195831703456429434E-14 ) ) ;
#958=EDGE_CURVE ( 'NONE', #7221, #4390, #202, .T. ) ;
#961=ORIENTED_EDGE ( 'NONE', *, *, #6276, .T. ) ;
#966=ADVANCED_FACE ( 'NONE', ( #6106 ), #1749, .T. ) ;
#968=CARTESIAN_POINT ( 'NONE',  ( 0.000000000000000000, 0.000000000000000000, -4.000000000000000000 ) ) ;
#978=CARTESIAN_POINT ( 'NONE',  ( 3.333333333333335702, -2.694301256218268215, -3.300726591567084256 ) ) ;
#995=CARTESIAN_POINT ( 'NONE',  ( -0.6448876103708541807, -4.246476118072358474, -0.2256878752776773356 ) ) ;
#998=( BOUNDED_SURFACE ( )  B_SPLINE_SURFACE ( 3, 2, ( 
 ( #5283, #2322, #5148 ),
 ( #1736, #3415, #1243 ),
 ( #2943, #6915, #4729 ),
 ( #4050, #1281, #3984 ),
 ( #166, #1832, #4025 ),
 ( #7018, #6939, #722 ) ),
 .UNSPECIFIED., .F., .F., .T. ) 
 B_SPLINE_SURFACE_WITH_KNOTS ( ( 4, 2, 4 ),
 ( 3, 3 ),
 ( 0.02032853247518125531, 0.02278863295364820865, 0.02524873343211516200 ),
 ( 0.000000000000000000, 1.000000000000000000 ),
 .UNSPECIFIED. ) 
 GEOMETRIC_REPRESENTATION_ITEM ( )  RATIONAL_B_SPLINE_SURFACE ( (
 ( 1.000000000000000000, 0.8047781615896836271, 1.000000000000000000),
 ( 1.000000000000000000, 0.8123767586289967202, 1.000000000000000000),
 ( 1.000000000000000000, 0.8190662415563443322, 1.000000000000000000),
 ( 1.000000000000000000, 0.8192361015669982205, 1.000000000000000000),
 ( 1.000000000000000000, 0.8126135807103181952, 1.000000000000000000),
 ( 1.000000000000000000, 0.8047712338318587788, 1.000000000000000000) ) ) 
 REPRESENTATION_ITEM ( '' )  SURFACE ( )  );
#1000=VERTEX_POINT ( 'NONE', #3845 ) ;
#1002=EDGE_CURVE ( 'NONE', #719, #853, #6743, .T. ) ;
#1013=CONICAL_SURFACE ( 'NONE', #1245, 5.560781378645573980, 1.221730476396046816 ) ;
#1016=LINE ( 'NONE', #3155, #2036 ) ;
#1021=EDGE_LOOP ( 'NONE', ( #1633, #1670, #6133, #3807 ) ) ;
#1028=CARTESIAN_POINT ( 'NONE',  ( 1.274258131564866448, 3.883108878240963513, -3.220599429844046568 ) ) ;
#1037=CARTESIAN_POINT ( 'NONE',  ( 4.000000000000000000, 2.309401076758515803, -0.4999999999999995559 ) ) ;
#1040=DIRECTION ( 'NONE',  ( -1.000000000000000000, 0.000000000000000000, 0.000000000000000000 ) ) ;
#1042=CARTESIAN_POINT ( 'NONE',  ( 2.548804901056335857E-15, 4.736522675502163437, -3.681124513963624612 ) ) ;
#1064=CARTESIAN_POINT ( 'NONE',  ( 1.287237434362044075, 3.875615274277557809, -3.430618716626812059 ) ) ;
#1068=DIRECTION ( 'NONE',  ( -1.000000000000000000, 0.000000000000000000, 0.000000000000000000 ) ) ;
#1085=LINE ( 'NONE', #2985, #6754 ) ;
#1092=AXIS2_PLACEMENT_3D ( 'NONE', #1591, #4402, #6129 ) ;
#1096=CARTESIAN_POINT ( 'NONE',  ( -0.1756481739660520902, 4.720212674038980261, -3.469390959564065291 ) ) ;
#1100=ORIENTED_EDGE ( 'NONE', *, *, #6031, .T. ) ;
#1106=( NAMED_UNIT ( * ) PLANE_ANGLE_UNIT ( ) SI_UNIT ( $, .RADIAN. ) );
#1108=CIRCLE ( 'NONE', #4667, 2.100000000000000089 ) ;
#1117=AXIS2_PLACEMENT_3D ( 'NONE', #1452, #308, #1420 ) ;
#1120=DIRECTION ( 'NONE',  ( 0.000000000000000000, 0.000000000000000000, 1.000000000000000000 ) ) ;
#1126=AXIS2_PLACEMENT_3D ( 'NONE', #4658, #5647, #5099 ) ;
#1135=DIRECTION ( 'NONE',  ( 0.000000000000000000, 0.000000000000000000, 1.000000000000000000 ) ) ;
#1136=DIRECTION ( 'NONE',  ( 0.000000000000000000, 0.000000000000000000, 1.000000000000000000 ) ) ;
#1140=DIRECTION ( 'NONE',  ( -0.000000000000000000, -0.000000000000000000, 1.000000000000000000 ) ) ;
#1144=COLOUR_RGB ( '',1.000000000000000000, 0.9490196078431372140, 0.9098039215686274384 ) ;
#1145=CARTESIAN_POINT ( 'NONE',  ( -2.688821387764050996E-14, -4.618802153517012954, -0.4999999999999995559 ) ) ;
#1149=CIRCLE ( 'NONE', #439, 5.560781378645573980 ) ;
#1150=CARTESIAN_POINT ( 'NONE',  ( -4.000000000000000000, 2.309401076758498483, -3.433295621305379353 ) ) ;
#1155=EDGE_LOOP ( 'NONE', ( #3247, #2570 ) ) ;
#1171=CARTESIAN_POINT ( 'NONE',  ( 0.000000000000000000, 0.000000000000000000, -5.000000000000000000 ) ) ;
#1172=CARTESIAN_POINT ( 'NONE',  ( 0.000000000000000000, 0.000000000000000000, -4.974599999999998801 ) ) ;
#1176=EDGE_CURVE ( 'NONE', #1728, #7233, #2230, .T. ) ;
#1186=ORIENTED_EDGE ( 'NONE', *, *, #2822, .T. ) ;
#1197=EDGE_CURVE ( 'NONE', #2273, #807, #6922, .T. ) ;
#1225=CARTESIAN_POINT ( 'NONE',  ( -2.855764796983342624, 2.970025579236414082, -0.09382832055445475272 ) ) ;
#1226=CARTESIAN_POINT ( 'NONE',  ( 4.000000000000000000, 2.309401076758497151, -5.000000000000000000 ) ) ;
#1232=CARTESIAN_POINT ( 'NONE',  ( 2.500000000000000888, 3.061616997868384127E-16, -4.974599999999998801 ) ) ;
#1234=CARTESIAN_POINT ( 'NONE',  ( 3.455068668934414777, -2.624017327439094327, -3.316620875263732504 ) ) ;
#1238=DIRECTION ( 'NONE',  ( -0.000000000000000000, -0.000000000000000000, 1.000000000000000000 ) ) ;
#1241=VERTEX_POINT ( 'NONE', #1259 ) ;
#1243=CARTESIAN_POINT ( 'NONE',  ( -0.6640947660597427138, 4.471078309994878985, -3.602146406945963442 ) ) ;
#1245=AXIS2_PLACEMENT_3D ( 'NONE', #4355, #5763, #637 ) ;
#1253=ORIENTED_EDGE ( 'NONE', *, *, #3381, .F. ) ;
#1259=CARTESIAN_POINT ( 'NONE',  ( -2.000000000000007550, -3.464101615137749945, 0.000000000000000000 ) ) ;
#1263=EDGE_CURVE ( 'NONE', #4634, #4692, #7317, .T. ) ;
#1272=ADVANCED_FACE ( 'NONE', ( #7029 ), #146, .F. ) ;
#1273=CARTESIAN_POINT ( 'NONE',  ( 1.411581201560190495E-15, 4.862606272033091592, -3.745885042887436622 ) ) ;
#1278=ORIENTED_EDGE ( 'NONE', *, *, #3591, .T. ) ;
#1281=CARTESIAN_POINT ( 'NONE',  ( -2.712762565639006418, 3.052587955997511759, -3.430618716626627318 ) ) ;
#1284=EDGE_CURVE ( 'NONE', #4530, #1949, #4744, .T. ) ;
#1288=VERTEX_POINT ( 'NONE', #3096 ) ;
#1302=CARTESIAN_POINT ( 'NONE',  ( -0.1750025118121544265, -4.719839900820635314, -3.469254087858253399 ) ) ;
#1310=CARTESIAN_POINT ( 'NONE',  ( -1.390230914382372118, -4.043987460488664532, -3.502507215260523665 ) ) ;
#1315=DIRECTION ( 'NONE',  ( -0.000000000000000000, -0.000000000000000000, 1.000000000000000000 ) ) ;
#1324=CARTESIAN_POINT ( 'NONE',  ( -4.000000000000000000, -0.8382240730041925492, -3.220610619767135141 ) ) ;
#1326=ADVANCED_FACE ( 'NONE', ( #2547 ), #1377, .F. ) ;
#1335=B_SPLINE_CURVE_WITH_KNOTS ( 'NONE', 3,
 ( #4464, #3784, #6084, #6684, #3242, #5589, #946, #5429 ),
 .UNSPECIFIED., .F., .F.,
 ( 4, 2, 2, 4 ),
 ( 2.465131517071610173E-07, 0.001183067374689837636, 0.001774477805458902699, 0.002365888236227967761 ),
 .UNSPECIFIED. ) ;
#1337=FACE_OUTER_BOUND ( 'NONE', #3306, .T. ) ;
#1345=ORIENTED_EDGE ( 'NONE', *, *, #6912, .T. ) ;
#1357=CIRCLE ( 'NONE', #5191, 2.100000000000000089 ) ;
#1358=CIRCLE ( 'NONE', #2670, 5.560781378645573980 ) ;
#1377=CONICAL_SURFACE ( 'NONE', #3408, 2.059999999999998721, 0.9599310885968738161 ) ;
#1380=CARTESIAN_POINT ( 'NONE',  ( 3.436319922986518449, -2.634841920959471562, -3.531542292954761741 ) ) ;
#1383=CARTESIAN_POINT ( 'NONE',  ( -1.391697335622809950, -4.043246145443391448, -3.503898532754372575 ) ) ;
#1390=CARTESIAN_POINT ( 'NONE',  ( 0.1410422978106145031, -4.700232962125109104, -3.687027686973628704 ) ) ;
#1409=CARTESIAN_POINT ( 'NONE',  ( -4.154094228333736538, -2.398367420967545627, -3.721909803043222276 ) ) ;
#1420=DIRECTION ( 'NONE',  ( -1.000000000000000000, 0.000000000000000000, 0.000000000000000000 ) ) ;
#1426=CARTESIAN_POINT ( 'NONE',  ( -4.000000000000000000, -0.3979232138631226823, -3.896351557369779711E-17 ) ) ;
#1452=CARTESIAN_POINT ( 'NONE',  ( 0.000000000000000000, 0.000000000000000000, 0.000000000000000000 ) ) ;
#1461=CARTESIAN_POINT ( 'NONE',  ( -4.000000000000000888, 1.563622288139195238, -0.2253451193528307472 ) ) ;
#1462=AXIS2_PLACEMENT_3D ( 'NONE', #2524, #428, #5496 ) ;
#1467=ORIENTED_EDGE ( 'NONE', *, *, #4714, .F. ) ;
#1470=AXIS2_PLACEMENT_3D ( 'NONE', #1940, #5854, #2498 ) ;
#1477=CARTESIAN_POINT ( 'NONE',  ( -3.974344831685191280E-13, 4.796734841935104576, -3.721909803043223608 ) ) ;
#1479=DIRECTION ( 'NONE',  ( -0.000000000000000000, -0.000000000000000000, 1.000000000000000000 ) ) ;
#1482=B_SPLINE_CURVE_WITH_KNOTS ( 'NONE', 3,
 ( #4505, #2730, #4571, #3324 ),
 .UNSPECIFIED., .F., .F.,
 ( 4, 4 ),
 ( 0.000000000000000000, 0.002452478801916361129 ),
 .UNSPECIFIED. ) ;
#1488=CONICAL_SURFACE ( 'NONE', #4955, 4.000000000000000000, 0.8911886515913786111 ) ;
#1494=CARTESIAN_POINT ( 'NONE',  ( 4.000000000000000000, -1.700175430507292473, -3.320327275037661785 ) ) ;
#1500=ORIENTED_EDGE ( 'NONE', *, *, #3316, .T. ) ;
#1518=EDGE_CURVE ( 'NONE', #3217, #1606, #2218, .T. ) ;
#1524=ORIENTED_EDGE ( 'NONE', *, *, #4932, .T. ) ;
#1526=ORIENTED_EDGE ( 'NONE', *, *, #4411, .F. ) ;
#1528=CARTESIAN_POINT ( 'NONE',  ( 2.499999999999999556, 0.000000000000000000, 3.469446951953614189E-15 ) ) ;
#1529=CARTESIAN_POINT ( 'NONE',  ( -4.101948962585906244, 2.368261337751074169, -3.681124513963621503 ) ) ;
#1539=CARTESIAN_POINT ( 'NONE',  ( -4.211140560182196957, 2.431303136016537803, -3.745885042887433514 ) ) ;
#1565=CARTESIAN_POINT ( 'NONE',  ( -4.024497503033519941, 2.323544716729375459, -3.572167766733379768 ) ) ;
#1573=DIRECTION ( 'NONE',  ( 1.000000000000000000, 0.000000000000000000, 0.000000000000000000 ) ) ;
#1575=EDGE_LOOP ( 'NONE', ( #2528, #2343, #3084, #1186, #7271, #6192, #1345 ) ) ;
#1580=CARTESIAN_POINT ( 'NONE',  ( 3.453038570460273071, 2.625189405340834448, -3.535263753543585352 ) ) ;
#1584=UNCERTAINTY_MEASURE_WITH_UNIT (LENGTH_MEASURE( 1.000000000000000082E-05 ), #6374, 'distance_accuracy_value', 'NONE');
#1591=CARTESIAN_POINT ( 'NONE',  ( 0.000000000000000000, 0.000000000000000000, -4.974599999999998801 ) ) ;
#1594=ORIENTED_EDGE ( 'NONE', *, *, #4111, .T. ) ;
#1602=B_SPLINE_CURVE_WITH_KNOTS ( 'NONE', 3,
 ( #5624, #1725, #4016, #6228, #6340 ),
 .UNSPECIFIED., .F., .F.,
 ( 4, 1, 4 ),
 ( 0.000000000000000000, 0.002309401076758505356, 0.004618802153517010713 ),
 .UNSPECIFIED. ) ;
#1606=VERTEX_POINT ( 'NONE', #5560 ) ;
#1609=FACE_OUTER_BOUND ( 'NONE', #2982, .T. ) ;
#1610=ADVANCED_FACE ( 'NONE', ( #7323 ), #998, .F. ) ;
#1622=DIRECTION ( 'NONE',  ( 1.000000000000000000, 0.000000000000000000, 0.000000000000000000 ) ) ;
#1633=ORIENTED_EDGE ( 'NONE', *, *, #7098, .F. ) ;
#1640=CARTESIAN_POINT ( 'NONE',  ( 2.500000000000000444, 0.000000000000000000, -25.03750572909317285 ) ) ;
#1659=ORIENTED_EDGE ( 'NONE', *, *, #727, .T. ) ;
#1670=ORIENTED_EDGE ( 'NONE', *, *, #575, .T. ) ;
#1672=CARTESIAN_POINT ( 'NONE',  ( 1.747541505913279281, -3.837784562140273081, -3.503702292528912299 ) ) ;
#1696=DIRECTION ( 'NONE',  ( -0.8191520442889902442, 0.000000000000000000, -0.5735764363510482688 ) ) ;
#1700=B_SPLINE_CURVE_WITH_KNOTS ( 'NONE', 3,
 ( #4240, #4281, #5938, #3063, #6571, #4202, #766, #5331 ),
 .UNSPECIFIED., .F., .F.,
 ( 4, 2, 2, 4 ),
 ( 7.780516681398759253E-20, 0.002450665683189819696, 0.003675998524784729327, 0.004901331366379639391 ),
 .UNSPECIFIED. ) ;
#1704=ORIENTED_EDGE ( 'NONE', *, *, #4846, .T. ) ;
#1708=( BOUNDED_SURFACE ( )  B_SPLINE_SURFACE ( 3, 2, ( 
 ( #5988, #6032, #375 ),
 ( #1494, #4936, #7073 ),
 ( #339, #1967, #6073 ),
 ( #848, #2638, #3106 ),
 ( #7224, #1921, #4220 ),
 ( #5649, #4004, #2235 ) ),
 .UNSPECIFIED., .F., .F., .T. ) 
 B_SPLINE_SURFACE_WITH_KNOTS ( ( 4, 2, 4 ),
 ( 3, 3 ),
 ( 0.02027065861071770947, 0.02273072267836921331, 0.02519078674602071716 ),
 ( 0.000000000000000000, 1.000000000000000000 ),
 .UNSPECIFIED. ) 
 GEOMETRIC_REPRESENTATION_ITEM ( )  RATIONAL_B_SPLINE_SURFACE ( (
 ( 1.000000000000000000, 0.8047781708337304885, 1.000000000000000000),
 ( 1.000000000000000000, 0.8123765190705307671, 1.000000000000000000),
 ( 1.000000000000000000, 0.8190656277163975707, 1.000000000000000000),
 ( 1.000000000000000000, 0.8192366903512159348, 1.000000000000000000),
 ( 1.000000000000000000, 0.8126138454302893610, 1.000000000000000000),
 ( 1.000000000000000000, 0.8047712246031417660, 1.000000000000000000) ) ) 
 REPRESENTATION_ITEM ( '' )  SURFACE ( )  );
#1725=CARTESIAN_POINT ( 'NONE',  ( 3.333333333333332593, 2.694301256218250007, -3.300726591567078483 ) ) ;
#1728=VERTEX_POINT ( 'NONE', #4651 ) ;
#1736=CARTESIAN_POINT ( 'NONE',  ( -0.5276280594146446346, 4.314175951381965746, -3.320322319201721495 ) ) ;
#1745=ORIENTED_EDGE ( 'NONE', *, *, #3426, .T. ) ;
#1749=CONICAL_SURFACE ( 'NONE', #87, 5.560781378645573980, 1.221730476396046816 ) ;
#1751=ADVANCED_FACE ( 'NONE', ( #2609 ), #4497, .F. ) ;
#1753=CARTESIAN_POINT ( 'NONE',  ( 0.000000000000000000, 0.000000000000000000, -4.000000000000000000 ) ) ;
#1754=ORIENTED_EDGE ( 'NONE', *, *, #3222, .F. ) ;
#1762=FACE_OUTER_BOUND ( 'NONE', #2193, .T. ) ;
#1795=CARTESIAN_POINT ( 'NONE',  ( -1.655952806101422814, 3.662737355149034979, -7.623296525288699970E-18 ) ) ;
#1802=PLANE ( 'NONE',  #4219 ) ;
#1805=CARTESIAN_POINT ( 'NONE',  ( -4.000000000000000000, 0.8730739991738342143, -3.223134629628428893 ) ) ;
#1806=AXIS2_PLACEMENT_3D ( 'NONE', #3314, #5613, #7267 ) ;
#1808=EDGE_CURVE ( 'NONE', #2174, #3114, #1962, .T. ) ;
#1818=FACE_OUTER_BOUND ( 'NONE', #7321, .T. ) ;
#1832=CARTESIAN_POINT ( 'NONE',  ( -3.436319922987618902, 2.634841920961291439, -3.531542292955721862 ) ) ;
#1835=CARTESIAN_POINT ( 'NONE',  ( 3.999999999999999112, 2.309401076758497595, -3.504271511726784194 ) ) ;
#1836=CARTESIAN_POINT ( 'NONE',  ( 1.734723475976807094E-15, 4.618802153517012954, -0.4999999999999995559 ) ) ;
#1839=STYLED_ITEM ( 'NONE', ( #5878 ), #4767 ) ;
#1848=CARTESIAN_POINT ( 'NONE',  ( -4.197312064133472020, -0.8182229787990021874, -3.502518405183886685 ) ) ;
#1849=ORIENTED_EDGE ( 'NONE', *, *, #1263, .T. ) ;
#1852=ADVANCED_FACE ( 'NONE', ( #6717 ), #4243, .F. ) ;
#1853=CIRCLE ( 'NONE', #6304, 2.500000000000000444 ) ;
#1861=SHAPE_REPRESENTATION_RELATIONSHIP ( 'NONE' , 'NONE' ,  #5023, #4767 ) ;
#1867=CARTESIAN_POINT ( 'NONE',  ( 4.000000000000000000, 2.309401076758497151, -3.433295621305379353 ) ) ;
#1879=CARTESIAN_POINT ( 'NONE',  ( -4.203934362469166963, -1.640673743454851286, -3.598432614606932756 ) ) ;
#1885=EDGE_CURVE ( 'NONE', #1000, #1976, #4456, .T. ) ;
#1886=DIRECTION ( 'NONE',  ( 1.000000000000000000, 0.000000000000000000, 0.000000000000000000 ) ) ;
#1896=CARTESIAN_POINT ( 'NONE',  ( -2.756197834950067094, -3.027510591568735254, -3.223146290109809797 ) ) ;
#1902=CARTESIAN_POINT ( 'NONE',  ( -4.000000000000000000, -2.309401076758515803, -0.4999999999999995559 ) ) ;
#1910=CARTESIAN_POINT ( 'NONE',  ( -4.000000000000000000, 2.471528634177585282, -3.686887442155186712 ) ) ;
#1916=ORIENTED_EDGE ( 'NONE', *, *, #5184, .F. ) ;
#1921=CARTESIAN_POINT ( 'NONE',  ( 4.000000000001088907, 1.658577278524410170, -3.531553309554541720 ) ) ;
#1926=( LENGTH_UNIT ( ) NAMED_UNIT ( * ) SI_UNIT ( .MILLI., .METRE. ) );
#1932=VERTEX_POINT ( 'NONE', #3940 ) ;
#1938=B_SPLINE_CURVE_WITH_KNOTS ( 'NONE', 3,
 ( #6690, #6092, #3707, #2660, #3171, #1037 ),
 .UNSPECIFIED., .F., .F.,
 ( 4, 2, 4 ),
 ( 0.002365888236227995517, 0.003551327329835084114, 0.004736766423442172712 ),
 .UNSPECIFIED. ) ;
#1940=CARTESIAN_POINT ( 'NONE',  ( 0.000000000000000000, 0.000000000000000000, 0.000000000000000000 ) ) ;
#1944=EDGE_CURVE ( 'NONE', #2273, #853, #4540, .T. ) ;
#1949=VERTEX_POINT ( 'NONE', #5705 ) ;
#1958=ORIENTED_EDGE ( 'NONE', *, *, #104, .T. ) ;
#1960=DIRECTION ( 'NONE',  ( 1.224646799147353207E-16, 1.000000000000000000, 0.000000000000000000 ) ) ;
#1962=B_SPLINE_CURVE_WITH_KNOTS ( 'NONE', 3,
 ( #3627, #5356, #3163, #3664, #5463, #351, #2494, #7084 ),
 .UNSPECIFIED., .F., .F.,
 ( 4, 2, 2, 4 ),
 ( 0.005725059856848645212, 0.006314084072593634418, 0.006903108288338624492, 0.008081156719828603771 ),
 .UNSPECIFIED. ) ;
#1963=AXIS2_PLACEMENT_3D ( 'NONE', #2294, #628, #5829 ) ;
#1967=CARTESIAN_POINT ( 'NONE',  ( 4.000000000000000888, -0.8578082829538523635, -3.433262215449808696 ) ) ;
#1976=VERTEX_POINT ( 'NONE', #580 ) ;
#1993=ADVANCED_FACE ( 'NONE', ( #5238, #711 ), #2836, .T. ) ;
#2001=DIRECTION ( 'NONE',  ( -0.000000000000000000, -0.000000000000000000, 1.000000000000000000 ) ) ;
#2005=ORIENTED_EDGE ( 'NONE', *, *, #5644, .T. ) ;
#2006=CARTESIAN_POINT ( 'NONE',  ( 1.411581201560190495E-15, 4.862606272033091592, -3.745885042887436622 ) ) ;
#2025=CIRCLE ( 'NONE', #1092, 2.500000000000000888 ) ;
#2031=CARTESIAN_POINT ( 'NONE',  ( -4.211140560182196957, 2.431303136016537803, -3.745885042887433514 ) ) ;
#2033=EDGE_CURVE ( 'NONE', #719, #214, #1853, .T. ) ;
#2035=ADVANCED_FACE ( 'NONE', ( #1818 ), #6066, .F. ) ;
#2036=VECTOR ( 'NONE', #2001, 1000.000000000000000 ) ;
#2042=ORIENTED_EDGE ( 'NONE', *, *, #184, .F. ) ;
#2048=EDGE_LOOP ( 'NONE', ( #4568, #1849, #5404, #4524, #1500 ) ) ;
#2050=CARTESIAN_POINT ( 'NONE',  ( 4.140404888673277384, 2.228338276487440428, -3.686887068327033390 ) ) ;
#2053=AXIS2_PLACEMENT_3D ( 'NONE', #162, #93, #6415 ) ;
#2054=PLANE ( 'NONE',  #412 ) ;
#2083=B_SPLINE_CURVE_WITH_KNOTS ( 'NONE', 3,
 ( #6546, #1409, #6620, #3682, #843, #3718 ),
 .UNSPECIFIED., .F., .F.,
 ( 4, 2, 4 ),
 ( -3.640115492409406142E-06, 0.0002066546034006526487, 0.0004169493222937146744 ),
 .UNSPECIFIED. ) ;
#2094=ORIENTED_EDGE ( 'NONE', *, *, #1518, .F. ) ;
#2128=ORIENTED_EDGE ( 'NONE', *, *, #958, .F. ) ;
#2154=EDGE_CURVE ( 'NONE', #3217, #5543, #1085, .T. ) ;
#2158=AXIS2_PLACEMENT_3D ( 'NONE', #399, #2583, #1040 ) ;
#2160=DIRECTION ( 'NONE',  ( -0.000000000000000000, 0.000000000000000000, -1.000000000000000000 ) ) ;
#2166=DIRECTION ( 'NONE',  ( 1.000000000000000000, 0.000000000000000000, 0.000000000000000000 ) ) ;
#2167=CARTESIAN_POINT ( 'NONE',  ( -0.02511973781850462134, 4.877415612947412882, -3.751298745799839462 ) ) ;
#2172=CARTESIAN_POINT ( 'NONE',  ( 0.000000000000000000, 0.000000000000000000, -4.484454397937119197 ) ) ;
#2174=VERTEX_POINT ( 'NONE', #6821 ) ;
#2175=CARTESIAN_POINT ( 'NONE',  ( -6.259644161404860030E-16, -4.618802153517027165, -3.433295621305388234 ) ) ;
#2177=CARTESIAN_POINT ( 'NONE',  ( 1.144235203016666258, 3.958177651039090250, -0.09382832055445661235 ) ) ;
#2181=ORIENTED_EDGE ( 'NONE', *, *, #3832, .T. ) ;
#2188=CONICAL_SURFACE ( 'NONE', #3494, 4.000000000000000000, 0.8911886515913786111 ) ;
#2193=EDGE_LOOP ( 'NONE', ( #2510, #5963, #5235, #192 ) ) ;
#2194=VECTOR ( 'NONE', #1136, 1000.000000000000000 ) ;
#2197=LINE ( 'NONE', #2723, #5096 ) ;
#2207=CARTESIAN_POINT ( 'NONE',  ( 0.5449313310647804220, 4.304185902836899835, -3.316620875263383894 ) ) ;
#2217=CARTESIAN_POINT ( 'NONE',  ( -4.000000000000000000, -2.309401076758512694, -3.433295621305382461 ) ) ;
#2218=LINE ( 'NONE', #6691, #442 ) ;
#2221=VECTOR ( 'NONE', #2375, 1000.000000000000114 ) ;
#2230=B_SPLINE_CURVE_WITH_KNOTS ( 'NONE', 3,
 ( #5645, #4528, #2231, #1672, #6250, #3388, #5689, #2989 ),
 .UNSPECIFIED., .F., .F.,
 ( 4, 2, 2, 4 ),
 ( 0.000000000000000000, 0.002450665683189819262, 0.003675998524784728893, 0.004901331366379639391 ),
 .UNSPECIFIED. ) ;
#2231=CARTESIAN_POINT ( 'NONE',  ( 2.805705207896068476, -3.226868319750173075, -3.503898532754370354 ) ) ;
#2235=CARTESIAN_POINT ( 'NONE',  ( 4.211405965630455661, 2.460463115436283932, -3.751298928144577882 ) ) ;
#2236=DIRECTION ( 'NONE',  ( 1.000000000000000000, 0.000000000000000000, 0.000000000000000000 ) ) ;
#2240=DIRECTION ( 'NONE',  ( -1.000000000000000000, 0.000000000000000000, 0.000000000000000000 ) ) ;
#2243=FACE_OUTER_BOUND ( 'NONE', #5727, .T. ) ;
#2244=CARTESIAN_POINT ( 'NONE',  ( 8.673617379884035472E-16, 4.618802153517012954, -5.000000000000000000 ) ) ;
#2254=CARTESIAN_POINT ( 'NONE',  ( -6.259644161404860030E-16, -4.618802153517027165, -5.000000000000000000 ) ) ;
#2255=ADVANCED_FACE ( 'NONE', ( #2299 ), #2921, .F. ) ;
#2256=ORIENTED_EDGE ( 'NONE', *, *, #2783, .T. ) ;
#2261=ADVANCED_FACE ( 'NONE', ( #4695 ), #1802, .T. ) ;
#2269=ORIENTED_EDGE ( 'NONE', *, *, #4580, .F. ) ;
#2273=VERTEX_POINT ( 'NONE', #7095 ) ;
#2287=CIRCLE ( 'NONE', #5881, 2.500000000000000444 ) ;
#2290=AXIS2_PLACEMENT_3D ( 'NONE', #6120, #2652, #4952 ) ;
#2294=CARTESIAN_POINT ( 'NONE',  ( 0.000000000000000000, 0.000000000000000000, 0.000000000000000000 ) ) ;
#2296=ORIENTED_EDGE ( 'NONE', *, *, #2956, .F. ) ;
#2299=FACE_OUTER_BOUND ( 'NONE', #3525, .T. ) ;
#2304=CARTESIAN_POINT ( 'NONE',  ( -4.211140560182196957, 2.431303136016537803, -3.745885042887433514 ) ) ;
#2321=CARTESIAN_POINT ( 'NONE',  ( 1.655952806101427033, -3.662737355149048302, -1.182683869819604841E-14 ) ) ;
#2322=CARTESIAN_POINT ( 'NONE',  ( 0.1404048886732821022, 4.699864953788070565, -3.686887068327037387 ) ) ;
#2340=ORIENTED_EDGE ( 'NONE', *, *, #1944, .T. ) ;
#2343=ORIENTED_EDGE ( 'NONE', *, *, #2647, .T. ) ;
#2344=DIRECTION ( 'NONE',  ( -0.000000000000000000, -0.000000000000000000, 1.000000000000000000 ) ) ;
#2346=CARTESIAN_POINT ( 'NONE',  ( 0.000000000000000000, 0.000000000000000000, -5.000000000000000888 ) ) ;
#2364=CARTESIAN_POINT ( 'NONE',  ( -0.6666666666666666297, -4.233901974057276973, -3.300726591567087365 ) ) ;
#2375=DIRECTION ( 'NONE',  ( 0.8191520442889902442, 1.003171929053522651E-16, -0.5735764363510482688 ) ) ;
#2376=CARTESIAN_POINT ( 'NONE',  ( 3.522875095019493141, -2.820352903225631369, -3.598441714920572299 ) ) ;
#2377=PLANE ( 'NONE',  #2800 ) ;
#2379=EDGE_CURVE ( 'NONE', #3960, #5816, #1700, .T. ) ;
#2388=CARTESIAN_POINT ( 'NONE',  ( -4.000000000000000000, -0.7890432684750890990, -0.04868663549882315533 ) ) ;
#2398=CARTESIAN_POINT ( 'NONE',  ( -6.259644161404860030E-16, -4.618802153517027165, -3.433295621305388234 ) ) ;
#2408=VECTOR ( 'NONE', #4551, 1000.000000000000000 ) ;
#2417=( NAMED_UNIT ( * ) PLANE_ANGLE_UNIT ( ) SI_UNIT ( $, .RADIAN. ) );
#2434=ORIENTED_EDGE ( 'NONE', *, *, #4111, .F. ) ;
#2440=CARTESIAN_POINT ( 'NONE',  ( -4.000000000000000000, -2.472261339043343220, -3.687027428081192326 ) ) ;
#2452=FACE_OUTER_BOUND ( 'NONE', #2762, .T. ) ;
#2453=AXIS2_PLACEMENT_3D ( 'NONE', #7061, #6329, #7170 ) ;
#2458=CARTESIAN_POINT ( 'NONE',  ( -4.211140560182196957, -2.431303136016552013, -3.745885042887436178 ) ) ;
#2460=ORIENTED_EDGE ( 'NONE', *, *, #7052, .T. ) ;
#2462=CARTESIAN_POINT ( 'NONE',  ( 4.000000000000000000, -2.309401076758514915, -3.433295621305383349 ) ) ;
#2463=CARTESIAN_POINT ( 'NONE',  ( 0.02511973781850649831, -4.877415612947427981, -3.751298745799844792 ) ) ;
#2466=CARTESIAN_POINT ( 'NONE',  ( 4.000000000000000000, 2.309401076758497151, -3.433295621305379353 ) ) ;
#2467=CARTESIAN_POINT ( 'NONE',  ( -1.240299975428134203E-15, -4.736529461165891242, -3.681130640444276292 ) ) ;
#2489=DIRECTION ( 'NONE',  ( -0.000000000000000000, -0.000000000000000000, 1.000000000000000000 ) ) ;
#2494=CARTESIAN_POINT ( 'NONE',  ( 3.999999999999999112, 1.941961291383486277, -0.3515519931180248192 ) ) ;
#2495=DIRECTION ( 'NONE',  ( -0.8191520442889875797, 1.003171929053519570E-16, 0.5735764363510522656 ) ) ;
#2498=DIRECTION ( 'NONE',  ( -1.000000000000000000, 0.000000000000000000, 0.000000000000000000 ) ) ;
#2510=ORIENTED_EDGE ( 'NONE', *, *, #1284, .T. ) ;
#2513=AXIS2_PLACEMENT_3D ( 'NONE', #7304, #2160, #6747 ) ;
#2524=CARTESIAN_POINT ( 'NONE',  ( 4.000000000000000000, 2.309401076758497151, -5.000000000000000000 ) ) ;
#2528=ORIENTED_EDGE ( 'NONE', *, *, #3035, .F. ) ;
#2529=ORIENTED_EDGE ( 'NONE', *, *, #2033, .F. ) ;
#2547=FACE_OUTER_BOUND ( 'NONE', #6767, .T. ) ;
#2548=ORIENTED_EDGE ( 'NONE', *, *, #6031, .F. ) ;
#2552=CARTESIAN_POINT ( 'NONE',  ( 0.000000000000000000, 0.000000000000000000, -4.694516984716113228 ) ) ;
#2559=ORIENTED_EDGE ( 'NONE', *, *, #3381, .T. ) ;
#2565=VERTEX_POINT ( 'NONE', #6724 ) ;
#2566=CARTESIAN_POINT ( 'NONE',  ( -0.3461262719736137305, 4.658553426539289610, -3.671615880910373608 ) ) ;
#2570=ORIENTED_EDGE ( 'NONE', *, *, #3757, .T. ) ;
#2583=DIRECTION ( 'NONE',  ( -0.000000000000000000, 0.000000000000000000, -1.000000000000000000 ) ) ;
#2595=CARTESIAN_POINT ( 'NONE',  ( 0.000000000000000000, 0.000000000000000000, 3.469446951953614189E-15 ) ) ;
#2609=FACE_OUTER_BOUND ( 'NONE', #6661, .T. ) ;
#2610=DIRECTION ( 'NONE',  ( 0.8191520442889875797, 0.000000000000000000, 0.5735764363510522656 ) ) ;
#2623=CARTESIAN_POINT ( 'NONE',  ( 4.000000000000000000, 2.309401076758515803, -0.4999999999999995559 ) ) ;
#2627=ORIENTED_EDGE ( 'NONE', *, *, #4404, .T. ) ;
#2638=CARTESIAN_POINT ( 'NONE',  ( 4.000000000000000888, 0.8228435280416209752, -3.430609588141487976 ) ) ;
#2647=EDGE_CURVE ( 'NONE', #76, #1728, #4384, .T. ) ;
#2649=CARTESIAN_POINT ( 'NONE',  ( 2.742827927723449299, 3.035229711104609596, -3.433252694550591233 ) ) ;
#2652=DIRECTION ( 'NONE',  ( 0.000000000000000000, -1.000000000000000000, 0.000000000000000000 ) ) ;
#2660=CARTESIAN_POINT ( 'NONE',  ( 3.349226789952652439, 2.685125164760731487, -0.2236248678334773199 ) ) ;
#2664=B_SPLINE_CURVE_WITH_KNOTS ( 'NONE', 3,
 ( #3373, #4625, #5674, #3478, #5780, #555 ),
 .UNSPECIFIED., .F., .F.,
 ( 4, 2, 4 ),
 ( 4.336808689942017736E-19, 0.0002095117440854729585, 0.0004190234881709454834 ),
 .UNSPECIFIED. ) ;
#2666=LINE ( 'NONE', #2744, #5896 ) ;
#2670=AXIS2_PLACEMENT_3D ( 'NONE', #5242, #1238, #688 ) ;
#2680=CARTESIAN_POINT ( 'NONE',  ( -4.000000000000000000, 2.309401076758498483, -3.433295621305379353 ) ) ;
#2685=CARTESIAN_POINT ( 'NONE',  ( 0.000000000000000000, 0.000000000000000000, 0.000000000000000000 ) ) ;
#2689=ORIENTED_EDGE ( 'NONE', *, *, #3035, .T. ) ;
#2694=CARTESIAN_POINT ( 'NONE',  ( 4.000000000000000000, 2.309401076758497151, -3.433295621305379353 ) ) ;
#2695=AXIS2_PLACEMENT_3D ( 'NONE', #1172, #4114, #3438 ) ;
#2698=CARTESIAN_POINT ( 'NONE',  ( -4.000000000000000000, 0.1981133338132459731, 2.096406544454392723E-17 ) ) ;
#2702=AXIS2_PLACEMENT_3D ( 'NONE', #2595, #4330, #3806 ) ;
#2703=ORIENTED_EDGE ( 'NONE', *, *, #3757, .F. ) ;
#2716=ADVANCED_FACE ( 'NONE', ( #1762 ), #6283, .T. ) ;
#2717=CARTESIAN_POINT ( 'NONE',  ( -4.000000000000004441, 2.309401076758496263, -3.504269196027523847 ) ) ;
#2722=CARTESIAN_POINT ( 'NONE',  ( 1.734723475976807094E-15, 4.618802153517012954, -0.4999999999999995559 ) ) ;
#2723=CARTESIAN_POINT ( 'NONE',  ( -5.560781378645573980, 0.000000000000000000, -4.000000000000000000 ) ) ;
#2730=CARTESIAN_POINT ( 'NONE',  ( 4.203833317240879275, 1.627343821129582979, -3.597273115243889929 ) ) ;
#2741=CARTESIAN_POINT ( 'NONE',  ( -0.3198814748697807464, -4.434118497892185040, -0.3507732604232532969 ) ) ;
#2744=CARTESIAN_POINT ( 'NONE',  ( 5.560781378645573980, 6.809993116116507654E-16, -4.000000000000000000 ) ) ;
#2762=EDGE_LOOP ( 'NONE', ( #6483, #2340, #5301, #2094 ) ) ;
#2767=LINE ( 'NONE', #19, #2194 ) ;
#2770=ADVANCED_FACE ( 'NONE', ( #7078 ), #5912, .F. ) ;
#2771=AXIS2_PLACEMENT_3D ( 'NONE', #148, #6538, #2855 ) ;
#2776=CARTESIAN_POINT ( 'NONE',  ( -2.000000000000007550, -3.464101615137749945, 0.000000000000000000 ) ) ;
#2783=EDGE_CURVE ( 'NONE', #1288, #431, #1358, .T. ) ;
#2793=AXIS2_PLACEMENT_3D ( 'NONE', #831, #3088, #3518 ) ;
#2800=AXIS2_PLACEMENT_3D ( 'NONE', #3618, #4151, #4182 ) ;
#2806=CONICAL_SURFACE ( 'NONE', #75, 4.000000000000000000, 0.8911886515913786111 ) ;
#2810=EDGE_LOOP ( 'NONE', ( #5349, #6944, #1467 ) ) ;
#2822=EDGE_CURVE ( 'NONE', #7233, #1000, #3749, .T. ) ;
#2836=PLANE ( 'NONE',  #789 ) ;
#2850=ORIENTED_EDGE ( 'NONE', *, *, #6068, .F. ) ;
#2853=ADVANCED_FACE ( 'NONE', ( #4121 ), #716, .F. ) ;
#2855=DIRECTION ( 'NONE',  ( 0.000000000000000000, 0.000000000000000000, 1.000000000000000000 ) ) ;
#2871=ORIENTED_EDGE ( 'NONE', *, *, #6234, .T. ) ;
#2880=CARTESIAN_POINT ( 'NONE',  ( -4.000000000000000888, -1.539600717839011201, -3.300726591567081591 ) ) ;
#2886=CARTESIAN_POINT ( 'NONE',  ( -3.999999999998910649, -1.658469974638591804, -3.531532913075256186 ) ) ;
#2889=EDGE_CURVE ( 'NONE', #4692, #709, #6810, .T. ) ;
#2890=CARTESIAN_POINT ( 'NONE',  ( 0.000000000000000000, 0.000000000000000000, 3.469446951953614189E-15 ) ) ;
#2904=AXIS2_PLACEMENT_3D ( 'NONE', #3726, #6708, #1573 ) ;
#2915=ADVANCED_FACE ( 'NONE', ( #3777 ), #7230, .T. ) ;
#2921=CYLINDRICAL_SURFACE ( 'NONE', #1126, 2.500000000000000444 ) ;
#2933=CYLINDRICAL_SURFACE ( 'NONE', #3953, 2.500000000000000444 ) ;
#2934=DIRECTION ( 'NONE',  ( 0.000000000000000000, -0.000000000000000000, 1.000000000000000000 ) ) ;
#2937=SURFACE_STYLE_USAGE ( .BOTH. , #3575 ) ;
#2943=CARTESIAN_POINT ( 'NONE',  ( -1.243802165048909503, 3.900692638707381921, -3.223146290109805800 ) ) ;
#2946=PLANE ( 'NONE',  #3989 ) ;
#2947=B_SPLINE_CURVE_WITH_KNOTS ( 'NONE', 3,
 ( #4009, #499, #3463, #5164, #605, #2304 ),
 .UNSPECIFIED., .F., .F.,
 ( 4, 2, 4 ),
 ( 0.002452478801916376308, 0.003676905084148007850, 0.004901331366379639391 ),
 .UNSPECIFIED. ) ;
#2952=CARTESIAN_POINT ( 'NONE',  ( -4.000000000000000000, -2.309401076758512694, -3.433295621305382461 ) ) ;
#2956=EDGE_CURVE ( 'NONE', #2565, #1241, #5182, .T. ) ;
#2959=CONICAL_SURFACE ( 'NONE', #7173, 2.500000000000000888, 0.9599310885968785900 ) ;
#2969=( NAMED_UNIT ( * ) SI_UNIT ( $, .STERADIAN. ) SOLID_ANGLE_UNIT ( ) );
#2975=DIRECTION ( 'NONE',  ( -1.000000000000000000, 0.000000000000000000, 0.000000000000000000 ) ) ;
#2980=EDGE_CURVE ( 'NONE', #3497, #3960, #4904, .T. ) ;
#2982=EDGE_LOOP ( 'NONE', ( #6462, #2434, #2548 ) ) ;
#2984=CIRCLE ( 'NONE', #2513, 4.000000000000000000 ) ;
#2985=CARTESIAN_POINT ( 'NONE',  ( -2.100000000000000089, 2.571758278209441957E-16, -5.000000000000000000 ) ) ;
#2989=CARTESIAN_POINT ( 'NONE',  ( -6.473970235329672780E-16, -4.862606272033106691, -3.745885042887442395 ) ) ;
#3008=CARTESIAN_POINT ( 'NONE',  ( -3.510273485745307287, -2.827716139362669967, -3.610536846335890004 ) ) ;
#3015=( GEOMETRIC_REPRESENTATION_CONTEXT ( 3 ) GLOBAL_UNCERTAINTY_ASSIGNED_CONTEXT ( ( #6467 ) ) GLOBAL_UNIT_ASSIGNED_CONTEXT ( ( #3830, #1106, #5150 ) ) REPRESENTATION_CONTEXT ( 'NONE', 'WORKASPACE' ) );
#3035=EDGE_CURVE ( 'NONE', #76, #1288, #2666, .T. ) ;
#3042=ORIENTED_EDGE ( 'NONE', *, *, #4932, .F. ) ;
#3047=( NAMED_UNIT ( * ) PLANE_ANGLE_UNIT ( ) SI_UNIT ( $, .RADIAN. ) );
#3055=CARTESIAN_POINT ( 'NONE',  ( -4.000000000000000000, -2.309401076758515803, -0.4999999999999995559 ) ) ;
#3057=CARTESIAN_POINT ( 'NONE',  ( -3.679171394226034675, -2.494631558665844739, -0.3503314178412558211 ) ) ;
#3058=CARTESIAN_POINT ( 'NONE',  ( -6.473970235329672780E-16, -4.862606272033106691, -3.745885042887442395 ) ) ;
#3063=CARTESIAN_POINT ( 'NONE',  ( 2.449848172108560096, 3.432307619358740514, -3.503702292528905637 ) ) ;
#3072=EDGE_CURVE ( 'NONE', #3960, #3899, #3839, .T. ) ;
#3084=ORIENTED_EDGE ( 'NONE', *, *, #1176, .T. ) ;
#3088=DIRECTION ( 'NONE',  ( 0.000000000000000000, 0.000000000000000000, -1.000000000000000000 ) ) ;
#3089=FACE_OUTER_BOUND ( 'NONE', #36, .T. ) ;
#3090=CARTESIAN_POINT ( 'NONE',  ( 0.000000000000000000, 0.000000000000000000, 0.000000000000000000 ) ) ;
#3096=CARTESIAN_POINT ( 'NONE',  ( 5.560781378645575757, 0.000000000000000000, -4.000000000000000000 ) ) ;
#3105=ADVANCED_FACE ( 'NONE', ( #7292 ), #6861, .T. ) ;
#3106=CARTESIAN_POINT ( 'NONE',  ( 4.197310751797292738, 0.8178363989516252985, -3.502498386812444409 ) ) ;
#3111=CARTESIAN_POINT ( 'NONE',  ( -0.6937372685066653943, 4.453844082567723461, -3.610536846335889116 ) ) ;
#3114=VERTEX_POINT ( 'NONE', #2623 ) ;
#3119=CARTESIAN_POINT ( 'NONE',  ( -4.000000000000000000, 2.309401076758498483, -0.4999999999999927280 ) ) ;
#3143=ORIENTED_EDGE ( 'NONE', *, *, #2154, .T. ) ;
#3148=CARTESIAN_POINT ( 'NONE',  ( 1.567478505476134606E-15, 4.618802153517012066, -3.433295621305382905 ) ) ;
#3151=ORIENTED_EDGE ( 'NONE', *, *, #4101, .T. ) ;
#3155=CARTESIAN_POINT ( 'NONE',  ( -2.500000000000000444, 3.061616997868383634E-16, -25.03750572909317285 ) ) ;
#3163=CARTESIAN_POINT ( 'NONE',  ( 4.000000000000000000, 0.3987449864460005378, -0.01220643443059817035 ) ) ;
#3169=CARTESIAN_POINT ( 'NONE',  ( -6.259644161404860030E-16, -4.618802153517027165, -3.433295621305388234 ) ) ;
#3171=CARTESIAN_POINT ( 'NONE',  ( 3.679171394226031122, 2.494631558665830973, -0.3503314178412474389 ) ) ;
#3187=ORIENTED_EDGE ( 'NONE', *, *, #6006, .F. ) ;
#3190=B_SPLINE_CURVE_WITH_KNOTS ( 'NONE', 3,
 ( #3055, #3630, #7085, #2388, #1426, #208 ),
 .UNSPECIFIED., .F., .F.,
 ( 4, 2, 4 ),
 ( 0.003358874760055550156, 0.004541967308452096383, 0.005725059856848641743 ),
 .UNSPECIFIED. ) ;
#3200=CARTESIAN_POINT ( 'NONE',  ( 4.000000000000000000, -2.309401076758516691, -0.4999999999999995559 ) ) ;
#3201=CARTESIAN_POINT ( 'NONE',  ( 0.6810597143197052450, 4.461075778259290914, -3.598441714920602053 ) ) ;
#3209=EDGE_CURVE ( 'NONE', #4692, #4184, #5221, .T. ) ;
#3217=VERTEX_POINT ( 'NONE', #5183 ) ;
#3222=EDGE_CURVE ( 'NONE', #7, #4634, #461, .T. ) ;
#3225=DIRECTION ( 'NONE',  ( 0.000000000000000000, 0.000000000000000000, -1.000000000000000000 ) ) ;
#3242=CARTESIAN_POINT ( 'NONE',  ( 2.687328764639642653, -3.067272167851299969, -0.05923475698271395140 ) ) ;
#3247=ORIENTED_EDGE ( 'NONE', *, *, #2033, .T. ) ;
#3264=AXIS2_PLACEMENT_3D ( 'NONE', #2685, #851, #6075 ) ;
#3271=CONICAL_SURFACE ( 'NONE', #3264, 4.000000000000000000, 0.8911886515913786111 ) ;
#3282=B_SPLINE_CURVE_WITH_KNOTS ( 'NONE', 3,
 ( #3874, #2741, #995, #5598, #5561, #5041, #445, #2776 ),
 .UNSPECIFIED., .F., .F.,
 ( 4, 2, 2, 4 ),
 ( 2.465131517390770070E-07, 0.001183067374689869946, 0.001774477805458935659, 0.002365888236228001588 ),
 .UNSPECIFIED. ) ;
#3284=EDGE_LOOP ( 'NONE', ( #6510, #3781, #2296, #1916, #2871, #4864 ) ) ;
#3296=ADVANCED_FACE ( 'NONE', ( #3089 ), #2946, .T. ) ;
#3297=ORIENTED_EDGE ( 'NONE', *, *, #4714, .T. ) ;
#3306=EDGE_LOOP ( 'NONE', ( #3556, #4286, #1526, #6324 ) ) ;
#3314=CARTESIAN_POINT ( 'NONE',  ( 0.000000000000000000, 0.000000000000000000, -4.974599999999998801 ) ) ;
#3316=EDGE_CURVE ( 'NONE', #1241, #5950, #6177, .T. ) ;
#3324=CARTESIAN_POINT ( 'NONE',  ( 4.197393957002303999, 7.772902908466098641E-14, -3.503767560748929810 ) ) ;
#3325=CARTESIAN_POINT ( 'NONE',  ( 4.175002511812151873, 2.208363329454889445, -3.469254087858244073 ) ) ;
#3338=EDGE_CURVE ( 'NONE', #3638, #4072, #410, .T. ) ;
#3347=VECTOR ( 'NONE', #65, 1000.000000000000000 ) ;
#3355=ORIENTED_EDGE ( 'NONE', *, *, #4235, .T. ) ;
#3363=CARTESIAN_POINT ( 'NONE',  ( 4.000000000000000000, -2.309401076758514915, -5.000000000000000000 ) ) ;
#3369=EDGE_LOOP ( 'NONE', ( #4610, #6448, #2269 ) ) ;
#3373=CARTESIAN_POINT ( 'NONE',  ( 4.000000000000000000, -2.309401076758514915, -3.433295621305383349 ) ) ;
#3381=EDGE_CURVE ( 'NONE', #4934, #5816, #6095, .T. ) ;
#3388=CARTESIAN_POINT ( 'NONE',  ( 0.6937372685066666156, -4.453844082567737672, -3.610536846335894445 ) ) ;
#3399=CARTESIAN_POINT ( 'NONE',  ( 2.500000000000000444, 0.000000000000000000, -5.000000000000000888 ) ) ;
#3408=AXIS2_PLACEMENT_3D ( 'NONE', #3761, #7137, #5367 ) ;
#3415=CARTESIAN_POINT ( 'NONE',  ( -0.5469614295416921346, 4.303013824936271270, -3.535263753543735454 ) ) ;
#3426=EDGE_CURVE ( 'NONE', #5543, #4390, #3665, .T. ) ;
#3438=DIRECTION ( 'NONE',  ( -1.000000000000000000, 0.000000000000000000, 0.000000000000000000 ) ) ;
#3463=CARTESIAN_POINT ( 'NONE',  ( -4.198928548860774157, 0.8158838809860065044, -3.526471437616918170 ) ) ;
#3478=CARTESIAN_POINT ( 'NONE',  ( 4.101954839143059139, -2.368264730582948285, -3.681130640444269631 ) ) ;
#3494=AXIS2_PLACEMENT_3D ( 'NONE', #4835, #868, #5892 ) ;
#3497=VERTEX_POINT ( 'NONE', #6565 ) ;
#3499=EDGE_CURVE ( 'NONE', #5950, #3638, #3190, .T. ) ;
#3508=FILL_AREA_STYLE ('',( #6413 ) ) ;
#3513=( BOUNDED_SURFACE ( )  B_SPLINE_SURFACE ( 3, 2, ( 
 ( #1302, #5809, #7040 ),
 ( #5378, #4717, #122 ),
 ( #4677, #6371, #7009 ),
 ( #4076, #4181, #4222 ),
 ( #1234, #1380, #2376 ),
 ( #3573, #6410, #3617 ) ),
 .UNSPECIFIED., .F., .F., .T. ) 
 B_SPLINE_SURFACE_WITH_KNOTS ( ( 4, 2, 4 ),
 ( 3, 3 ),
 ( 0.02032853247518126918, 0.02278863295364821906, 0.02524873343211517240 ),
 ( 0.000000000000000000, 1.000000000000000000 ),
 .UNSPECIFIED. ) 
 GEOMETRIC_REPRESENTATION_ITEM ( )  RATIONAL_B_SPLINE_SURFACE ( (
 ( 1.000000000000000000, 0.8047781615896837382, 1.000000000000000000),
 ( 1.000000000000000000, 0.8123767586289252218, 1.000000000000000000),
 ( 1.000000000000000000, 0.8190662415564388121, 1.000000000000000000),
 ( 1.000000000000000000, 0.8192361015669026303, 1.000000000000000000),
 ( 1.000000000000000000, 0.8126135807103900266, 1.000000000000000000),
 ( 1.000000000000000000, 0.8047712338318593339, 1.000000000000000000) ) ) 
 REPRESENTATION_ITEM ( '' )  SURFACE ( )  );
#3518=DIRECTION ( 'NONE',  ( 1.000000000000000000, 0.000000000000000000, 0.000000000000000000 ) ) ;
#3525=EDGE_LOOP ( 'NONE', ( #417, #2529, #163, #5602 ) ) ;
#3550=CARTESIAN_POINT ( 'NONE',  ( 1.567478505476134606E-15, 4.618802153517012066, -5.000000000000000000 ) ) ;
#3556=ORIENTED_EDGE ( 'NONE', *, *, #511, .T. ) ;
#3564=ORIENTED_EDGE ( 'NONE', *, *, #3222, .T. ) ;
#3569=EDGE_CURVE ( 'NONE', #6701, #2565, #1335, .T. ) ;
#3571=DIRECTION ( 'NONE',  ( -1.000000000000000000, 0.000000000000000000, 0.000000000000000000 ) ) ;
#3573=CARTESIAN_POINT ( 'NONE',  ( 4.175648173966055587, -2.207990556236547608, -3.469390959564065291 ) ) ;
#3575=SURFACE_SIDE_STYLE ('',( #3619 ) ) ;
#3585=CARTESIAN_POINT ( 'NONE',  ( -0.6810597143197697489, -4.461075778259609770, -3.598441714920717516 ) ) ;
#3590=CARTESIAN_POINT ( 'NONE',  ( -1.240299975428113101E-15, -4.647091401871173311, -3.572172305156514849 ) ) ;
#3591=EDGE_CURVE ( 'NONE', #807, #7221, #6759, .T. ) ;
#3606=AXIS2_PLACEMENT_3D ( 'NONE', #7207, #6695, #362 ) ;
#3613=TOROIDAL_SURFACE ( 'NONE', #6154, 5.384454397937118664, 0.5155456020628804703 ) ;
#3617=CARTESIAN_POINT ( 'NONE',  ( 4.236525694536557474, -2.416953475386482530, -3.751298745799839462 ) ) ;
#3618=CARTESIAN_POINT ( 'NONE',  ( -6.259644161404860030E-16, -4.618802153517027165, -5.000000000000000000 ) ) ;
#3619=SURFACE_STYLE_FILL_AREA ( #3508 ) ;
#3620=APPLICATION_CONTEXT ( 'automotive_design' ) ;
#3624=ORIENTED_EDGE ( 'NONE', *, *, #3790, .F. ) ;
#3627=CARTESIAN_POINT ( 'NONE',  ( 4.000000000000000000, 0.000000000000000000, 0.000000000000000000 ) ) ;
#3630=CARTESIAN_POINT ( 'NONE',  ( -4.000000000000000000, -1.942223658245633811, -0.3516579909967644246 ) ) ;
#3632=CARTESIAN_POINT ( 'NONE',  ( -2.000000000000007550, -3.464101615137749945, 0.000000000000000000 ) ) ;
#3638=VERTEX_POINT ( 'NONE', #4998 ) ;
#3645=ORIENTED_EDGE ( 'NONE', *, *, #3072, .T. ) ;
#3648=EDGE_CURVE ( 'NONE', #4530, #1288, #396, .T. ) ;
#3664=CARTESIAN_POINT ( 'NONE',  ( 4.000000000000000000, 0.7924765000094659007, -0.05906175389889852662 ) ) ;
#3665=LINE ( 'NONE', #7019, #872 ) ;
#3680=ORIENTED_EDGE ( 'NONE', *, *, #511, .F. ) ;
#3682=CARTESIAN_POINT ( 'NONE',  ( -4.024497503033519941, -2.323544716729390558, -3.572167766733381544 ) ) ;
#3693=CARTESIAN_POINT ( 'NONE',  ( -3.511755186886750479, 2.826662030176366081, -3.597382984111578086 ) ) ;
#3699=CARTESIAN_POINT ( 'NONE',  ( -2.836893136758495970, -3.208949435745868328, -3.505054077164885484 ) ) ;
#3707=CARTESIAN_POINT ( 'NONE',  ( 2.682243648011666703, 3.070208061305304881, -0.04852650426601266831 ) ) ;
#3710=CARTESIAN_POINT ( 'NONE',  ( -2.345747346278108214, 3.264484291692489215, -0.01223254789873409049 ) ) ;
#3718=CARTESIAN_POINT ( 'NONE',  ( -4.000000000000000000, -2.309401076758512694, -3.433295621305382461 ) ) ;
#3725=CARTESIAN_POINT ( 'NONE',  ( 8.673617379884035472E-16, 4.618802153517012954, 0.000000000000000000 ) ) ;
#3726=CARTESIAN_POINT ( 'NONE',  ( 0.000000000000000000, 0.000000000000000000, -0.2800830152838844622 ) ) ;
#3749=B_SPLINE_CURVE_WITH_KNOTS ( 'NONE', 3,
 ( #125, #6447, #1383, #5211, #4755, #3008, #4226, #2458 ),
 .UNSPECIFIED., .F., .F.,
 ( 4, 2, 2, 4 ),
 ( 0.000000000000000000, 0.002450665683189818828, 0.003675998524784728459, 0.004901331366379638524 ),
 .UNSPECIFIED. ) ;
#3757=EDGE_CURVE ( 'NONE', #214, #719, #2287, .T. ) ;
#3761=CARTESIAN_POINT ( 'NONE',  ( 0.000000000000000000, 0.000000000000000000, -0.3080913168122742518 ) ) ;
#3772=FACE_OUTER_BOUND ( 'NONE', #3284, .T. ) ;
#3777=FACE_OUTER_BOUND ( 'NONE', #6330, .T. ) ;
#3781=ORIENTED_EDGE ( 'NONE', *, *, #4101, .F. ) ;
#3784=CARTESIAN_POINT ( 'NONE',  ( 3.680118525130245732, -2.494084732383344605, -0.3507732604232533524 ) ) ;
#3785=CARTESIAN_POINT ( 'NONE',  ( -4.000000000000000000, 0.9868501483902560878, -0.09357334158579519445 ) ) ;
#3790=EDGE_CURVE ( 'NONE', #709, #6701, #6266, .T. ) ;
#3795=CARTESIAN_POINT ( 'NONE',  ( 1.567478505476135000E-15, 4.618802153517012954, -3.504269196027527844 ) ) ;
#3806=DIRECTION ( 'NONE',  ( 1.000000000000000000, 0.000000000000000000, 0.000000000000000000 ) ) ;
#3807=ORIENTED_EDGE ( 'NONE', *, *, #6912, .F. ) ;
#3816=EDGE_LOOP ( 'NONE', ( #6576, #4815, #493, #4325, #3297 ) ) ;
#3830=( LENGTH_UNIT ( ) NAMED_UNIT ( * ) SI_UNIT ( .MILLI., .METRE. ) );
#3831=AXIS2_PLACEMENT_3D ( 'NONE', #470, #5703, #1068 ) ;
#3832=EDGE_CURVE ( 'NONE', #4934, #3899, #1602, .T. ) ;
#3839=B_SPLINE_CURVE_WITH_KNOTS ( 'NONE', 3,
 ( #4405, #1477, #1042, #4921, #3795, #4438 ),
 .UNSPECIFIED., .F., .F.,
 ( 4, 2, 4 ),
 ( -3.640115492407174633E-06, 0.0002066546034006553863, 0.0004169493222937179812 ),
 .UNSPECIFIED. ) ;
#3845=CARTESIAN_POINT ( 'NONE',  ( -4.211140560182196957, -2.431303136016552013, -3.745885042887436178 ) ) ;
#3846=ORIENTED_EDGE ( 'NONE', *, *, #4163, .F. ) ;
#3847=AXIS2_PLACEMENT_3D ( 'NONE', #3725, #7225, #6552 ) ;
#3848=CARTESIAN_POINT ( 'NONE',  ( -2.100000000000000089, 2.571758278209441957E-16, -0.2800830152838844622 ) ) ;
#3874=CARTESIAN_POINT ( 'NONE',  ( -2.688821387764050996E-14, -4.618802153517012954, -0.4999999999999995559 ) ) ;
#3877=APPLICATION_CONTEXT ( 'automotive_design' ) ;
#3899=VERTEX_POINT ( 'NONE', #4784 ) ;
#3902=DIRECTION ( 'NONE',  ( 0.000000000000000000, 0.000000000000000000, 1.000000000000000000 ) ) ;
#3904=CARTESIAN_POINT ( 'NONE',  ( 2.756197834950227410, 3.027510591568626896, -3.223146290109805356 ) ) ;
#3912=ORIENTED_EDGE ( 'NONE', *, *, #2379, .T. ) ;
#3915=DIRECTION ( 'NONE',  ( -1.000000000000000000, 0.000000000000000000, 0.000000000000000000 ) ) ;
#3935=CARTESIAN_POINT ( 'NONE',  ( 4.000000000000000000, -2.309401076758514915, -3.433295621305383349 ) ) ;
#3940=CARTESIAN_POINT ( 'NONE',  ( 2.000000000000008882, 3.464101615137749945, 0.000000000000000000 ) ) ;
#3946=ADVANCED_FACE ( 'NONE', ( #1337 ), #3513, .F. ) ;
#3948=CARTESIAN_POINT ( 'NONE',  ( 0.6507732100473444525, -4.243078065514795050, -0.2236248678334952777 ) ) ;
#3953=AXIS2_PLACEMENT_3D ( 'NONE', #6407, #2344, #1886 ) ;
#3960=VERTEX_POINT ( 'NONE', #1273 ) ;
#3966=CARTESIAN_POINT ( 'NONE',  ( -4.000000000000000000, 2.309401076758498483, -5.000000000000000000 ) ) ;
#3984=CARTESIAN_POINT ( 'NONE',  ( -2.807080416178626692, 3.225969019225154444, -3.502507215260441065 ) ) ;
#3989=AXIS2_PLACEMENT_3D ( 'NONE', #6427, #5249, #5392 ) ;
#3995=ORIENTED_EDGE ( 'NONE', *, *, #2647, .F. ) ;
#4004=CARTESIAN_POINT ( 'NONE',  ( 3.999999999999998224, 2.472263674411418588, -3.687027874309861897 ) ) ;
#4005=DIRECTION ( 'NONE',  ( -1.000000000000000000, 0.000000000000000000, 0.000000000000000000 ) ) ;
#4009=CARTESIAN_POINT ( 'NONE',  ( -4.197393957002303999, -7.773935952363655451E-14, -3.503767560748929810 ) ) ;
#4016=CARTESIAN_POINT ( 'NONE',  ( 2.000000000000000444, 3.464101615137754830, -3.142992957459231018 ) ) ;
#4025=CARTESIAN_POINT ( 'NONE',  ( -3.522875095019672109, 2.820352903225427532, -3.598441714920591394 ) ) ;
#4026=CARTESIAN_POINT ( 'NONE',  ( -2.499999999999999556, 3.061616997868382648E-16, 3.469446951953614189E-15 ) ) ;
#4028=CARTESIAN_POINT ( 'NONE',  ( -3.999999999999999112, 1.539600717838996324, -3.300726591567078039 ) ) ;
#4030=ORIENTED_EDGE ( 'NONE', *, *, #3832, .F. ) ;
#4040=CARTESIAN_POINT ( 'NONE',  ( -4.000000000000000000, 2.309401076758498483, -0.4999999999999927280 ) ) ;
#4050=CARTESIAN_POINT ( 'NONE',  ( -2.725741868435985094, 3.045094352034055429, -3.220599429844047012 ) ) ;
#4058=ADVANCED_FACE ( 'NONE', ( #4296, #3772 ), #4986, .F. ) ;
#4060=CARTESIAN_POINT ( 'NONE',  ( 2.100000000000000089, 0.000000000000000000, -5.000000000000000000 ) ) ;
#4072=VERTEX_POINT ( 'NONE', #6146 ) ;
#4076=CARTESIAN_POINT ( 'NONE',  ( 2.725741868436127202, -3.045094352033990148, -3.220599429844051453 ) ) ;
#4078=EDGE_CURVE ( 'NONE', #214, #1606, #1016, .T. ) ;
#4086=CARTESIAN_POINT ( 'NONE',  ( -1.317756351988340180, 3.857995168970202116, -0.04852650426601388955 ) ) ;
#4101=EDGE_CURVE ( 'NONE', #1241, #3638, #2984, .T. ) ;
#4111=EDGE_CURVE ( 'NONE', #5639, #1932, #7324, .T. ) ;
#4113=DIRECTION ( 'NONE',  ( 0.000000000000000000, 0.000000000000000000, -1.000000000000000000 ) ) ;
#4114=DIRECTION ( 'NONE',  ( 0.000000000000000000, 0.000000000000000000, -1.000000000000000000 ) ) ;
#4121=FACE_OUTER_BOUND ( 'NONE', #904, .T. ) ;
#4151=DIRECTION ( 'NONE',  ( 0.5000000000000013323, -0.8660254037844379305, 0.000000000000000000 ) ) ;
#4156=MECHANICAL_DESIGN_GEOMETRIC_PRESENTATION_REPRESENTATION('',(#1839),#170);
#4160=CARTESIAN_POINT ( 'NONE',  ( -3.472371940586054251, -2.614027278893156669, -3.320322319202162031 ) ) ;
#4163=EDGE_CURVE ( 'NONE', #3217, #2273, #1108, .T. ) ;
#4165=DIRECTION ( 'NONE',  ( 1.000000000000000000, 0.000000000000000000, 0.000000000000000000 ) ) ;
#4175=DIRECTION ( 'NONE',  ( -0.000000000000000000, -0.000000000000000000, 1.000000000000000000 ) ) ;
#4181=CARTESIAN_POINT ( 'NONE',  ( 2.712762565639649015, -3.052587955997662306, -3.430618716626630871 ) ) ;
#4182=DIRECTION ( 'NONE',  ( 0.8660254037844379305, 0.5000000000000013323, 0.000000000000000000 ) ) ;
#4184=VERTEX_POINT ( 'NONE', #6728 ) ;
#4192=CARTESIAN_POINT ( 'NONE',  ( -4.140404888673278272, -2.228338276487456415, -3.686887068327035166 ) ) ;
#4202=CARTESIAN_POINT ( 'NONE',  ( 3.510273485745307731, 2.827716139362654424, -3.610536846335885564 ) ) ;
#4214=ORIENTED_EDGE ( 'NONE', *, *, #4404, .F. ) ;
#4219=AXIS2_PLACEMENT_3D ( 'NONE', #3966, #699, #6252 ) ;
#4220=CARTESIAN_POINT ( 'NONE',  ( 4.203935335434060505, 1.640780671294165272, -3.598452447879202598 ) ) ;
#4222=CARTESIAN_POINT ( 'NONE',  ( 2.807080416178989513, -3.225969019225150003, -3.502507215260505014 ) ) ;
#4226=CARTESIAN_POINT ( 'NONE',  ( -3.861362476283256129, -2.629030857716004199, -3.671615880910374941 ) ) ;
#4235=EDGE_CURVE ( 'NONE', #1606, #853, #2025, .T. ) ;
#4240=CARTESIAN_POINT ( 'NONE',  ( 1.411581201560190495E-15, 4.862606272033091592, -3.745885042887436622 ) ) ;
#4242=CARTESIAN_POINT ( 'NONE',  ( 1.734723475976807094E-15, 4.618802153517012954, -0.4999999999999995559 ) ) ;
#4243=( BOUNDED_SURFACE ( )  B_SPLINE_SURFACE ( 3, 2, ( 
 ( #3325, #2050, #386 ),
 ( #6198, #1580, #504 ),
 ( #3904, #2649, #4348 ),
 ( #1028, #1064, #4951 ),
 ( #2207, #7236, #3201 ),
 ( #1096, #6758, #2167 ) ),
 .UNSPECIFIED., .F., .F., .F. ) 
 B_SPLINE_SURFACE_WITH_KNOTS ( ( 4, 2, 4 ),
 ( 3, 3 ),
 ( 0.02032853247518126225, 0.02278863295364821212, 0.02524873343211516200 ),
 ( 0.000000000000000000, 1.000000000000000000 ),
 .UNSPECIFIED. ) 
 GEOMETRIC_REPRESENTATION_ITEM ( )  RATIONAL_B_SPLINE_SURFACE ( (
 ( 1.000000000000000000, 0.8047781615896835161, 1.000000000000000000),
 ( 1.000000000000000000, 0.8123767586291043008, 1.000000000000000000),
 ( 1.000000000000000000, 0.8190662415562011134, 1.000000000000000000),
 ( 1.000000000000000000, 0.8192361015671398849, 1.000000000000000000),
 ( 1.000000000000000000, 0.8126135807102121689, 1.000000000000000000),
 ( 1.000000000000000000, 0.8047712338318585568, 1.000000000000000000) ) ) 
 REPRESENTATION_ITEM ( '' )  SURFACE ( )  );
#4247=EDGE_CURVE ( 'NONE', #4184, #1241, #3282, .T. ) ;
#4281=CARTESIAN_POINT ( 'NONE',  ( 0.6920835326022565237, 4.454600218803884459, -3.597382984111579862 ) ) ;
#4286=ORIENTED_EDGE ( 'NONE', *, *, #1176, .F. ) ;
#4296=FACE_BOUND ( 'NONE', #6592, .T. ) ;
#4323=ORIENTED_EDGE ( 'NONE', *, *, #1518, .T. ) ;
#4325=ORIENTED_EDGE ( 'NONE', *, *, #3569, .T. ) ;
#4329=CARTESIAN_POINT ( 'NONE',  ( -3.333333333333335258, 2.694301256218251783, -3.300726591567079815 ) ) ;
#4330=DIRECTION ( 'NONE',  ( -0.000000000000000000, -0.000000000000000000, 1.000000000000000000 ) ) ;
#4348=CARTESIAN_POINT ( 'NONE',  ( 2.836893136758676270, 3.208949435745843903, -3.505054077164911241 ) ) ;
#4355=CARTESIAN_POINT ( 'NONE',  ( 0.000000000000000000, 0.000000000000000000, -4.000000000000000000 ) ) ;
#4384=B_SPLINE_CURVE_WITH_KNOTS ( 'NONE', 3,
 ( #614, #6911, #5175, #549, #5775, #4468 ),
 .UNSPECIFIED., .F., .F.,
 ( 4, 2, 4 ),
 ( 0.002452478801916361129, 0.003676905084148001344, 0.004901331366379641126 ),
 .UNSPECIFIED. ) ;
#4390=VERTEX_POINT ( 'NONE', #4026 ) ;
#4402=DIRECTION ( 'NONE',  ( -0.000000000000000000, -0.000000000000000000, 1.000000000000000000 ) ) ;
#4404=EDGE_CURVE ( 'NONE', #7, #5278, #5745, .T. ) ;
#4405=CARTESIAN_POINT ( 'NONE',  ( 1.411581201560190495E-15, 4.862606272033091592, -3.745885042887436622 ) ) ;
#4407=EDGE_LOOP ( 'NONE', ( #2559, #5403, #3645, #4030 ) ) ;
#4411=EDGE_CURVE ( 'NONE', #709, #1728, #2664, .T. ) ;
#4412=PRODUCT_DEFINITION_SHAPE ( 'NONE', 'NONE',  #213 ) ;
#4417=B_SPLINE_CURVE_WITH_KNOTS ( 'NONE', 3,
 ( #436, #2698, #864, #7124, #3785, #1461, #7240, #3119 ),
 .UNSPECIFIED., .F., .F.,
 ( 4, 2, 2, 4 ),
 ( 0.005725059856848641743, 0.006314084072593626612, 0.006903108288338611481, 0.008081156719828581220 ),
 .UNSPECIFIED. ) ;
#4426=CARTESIAN_POINT ( 'NONE',  ( -4.211140560182196957, -2.431303136016552013, -3.745885042887436178 ) ) ;
#4427=CARTESIAN_POINT ( 'NONE',  ( 2.059999999999998721, 0.000000000000000000, -0.3080913168122742518 ) ) ;
#4438=CARTESIAN_POINT ( 'NONE',  ( 1.567478505476134606E-15, 4.618802153517012066, -3.433295621305382905 ) ) ;
#4453=CARTESIAN_POINT ( 'NONE',  ( 0.6448876103708359731, 4.246476118072354922, -0.2256878752776725616 ) ) ;
#4456=B_SPLINE_CURVE_WITH_KNOTS ( 'NONE', 3,
 ( #4426, #5068, #5236, #6119 ),
 .UNSPECIFIED., .F., .F.,
 ( 4, 4 ),
 ( 0.000000000000000000, 0.002452478801916376308 ),
 .UNSPECIFIED. ) ;
#4464=CARTESIAN_POINT ( 'NONE',  ( 4.000000000000000000, -2.309401076758516691, -0.4999999999999995559 ) ) ;
#4468=CARTESIAN_POINT ( 'NONE',  ( 4.211140560182196957, -2.431303136016555122, -3.745885042887436622 ) ) ;
#4469=ORIENTED_EDGE ( 'NONE', *, *, #5094, .T. ) ;
#4472=EDGE_LOOP ( 'NONE', ( #3624, #1704, #2460, #5883, #3042 ) ) ;
#4487=( GEOMETRIC_REPRESENTATION_CONTEXT ( 3 ) GLOBAL_UNCERTAINTY_ASSIGNED_CONTEXT ( ( #1584 ) ) GLOBAL_UNIT_ASSIGNED_CONTEXT ( ( #6374, #2417, #686 ) ) REPRESENTATION_CONTEXT ( 'NONE', 'WORKASPACE' ) );
#4495=DIRECTION ( 'NONE',  ( -0.9396926207859138680, 0.000000000000000000, -0.3420201433256536139 ) ) ;
#4497=( BOUNDED_SURFACE ( )  B_SPLINE_SURFACE ( 3, 2, ( 
 ( #7049, #4192, #273 ),
 ( #4160, #6451, #829 ),
 ( #1896, #6596, #3699 ),
 ( #7122, #752, #1310 ),
 ( #207, #4792, #3585 ),
 ( #5886, #1390, #2463 ) ),
 .UNSPECIFIED., .F., .F., .T. ) 
 B_SPLINE_SURFACE_WITH_KNOTS ( ( 4, 2, 4 ),
 ( 3, 3 ),
 ( 0.02032853247518126918, 0.02278863295364821906, 0.02524873343211516893 ),
 ( 0.000000000000000000, 1.000000000000000000 ),
 .UNSPECIFIED. ) 
 GEOMETRIC_REPRESENTATION_ITEM ( )  RATIONAL_B_SPLINE_SURFACE ( (
 ( 1.000000000000000000, 0.8047781615896838492, 1.000000000000000000),
 ( 1.000000000000000000, 0.8123767586288186404, 1.000000000000000000),
 ( 1.000000000000000000, 0.8190662415565814758, 1.000000000000000000),
 ( 1.000000000000000000, 0.8192361015667604107, 1.000000000000000000),
 ( 1.000000000000000000, 0.8126135807104967190, 1.000000000000000000),
 ( 1.000000000000000000, 0.8047712338318580017, 1.000000000000000000) ) ) 
 REPRESENTATION_ITEM ( '' )  SURFACE ( )  );
#4503=ORIENTED_EDGE ( 'NONE', *, *, #1197, .F. ) ;
#4505=CARTESIAN_POINT ( 'NONE',  ( 4.211140560182196957, 2.431303136016536470, -3.745885042887433514 ) ) ;
#4524=ORIENTED_EDGE ( 'NONE', *, *, #4247, .T. ) ;
#4528=CARTESIAN_POINT ( 'NONE',  ( 3.511755186886750923, -2.826662030176382956, -3.597382984111582083 ) ) ;
#4530=VERTEX_POINT ( 'NONE', #4876 ) ;
#4533=DIRECTION ( 'NONE',  ( -0.000000000000000000, -0.000000000000000000, 1.000000000000000000 ) ) ;
#4540=LINE ( 'NONE', #1232, #2221 ) ;
#4551=DIRECTION ( 'NONE',  ( 0.000000000000000000, 0.000000000000000000, 1.000000000000000000 ) ) ;
#4568=ORIENTED_EDGE ( 'NONE', *, *, #6276, .F. ) ;
#4571=CARTESIAN_POINT ( 'NONE',  ( 4.197393957002303999, 0.8151795401431359833, -3.503767560748935139 ) ) ;
#4580=EDGE_CURVE ( 'NONE', #1932, #3114, #1938, .T. ) ;
#4601=CIRCLE ( 'NONE', #296, 4.000000000000000000 ) ;
#4610=ORIENTED_EDGE ( 'NONE', *, *, #6234, .F. ) ;
#4623=CARTESIAN_POINT ( 'NONE',  ( 1.317756351988342622, -3.857995168970215438, -0.04852650426602527628 ) ) ;
#4625=CARTESIAN_POINT ( 'NONE',  ( 4.000000000000003553, -2.309401076758513138, -3.504271511726786859 ) ) ;
#4634=VERTEX_POINT ( 'NONE', #2217 ) ;
#4647=ORIENTED_EDGE ( 'NONE', *, *, #7052, .F. ) ;
#4648=CARTESIAN_POINT ( 'NONE',  ( 0.000000000000000000, 0.000000000000000000, -0.3080913168122742518 ) ) ;
#4651=CARTESIAN_POINT ( 'NONE',  ( 4.211140560182196957, -2.431303136016555122, -3.745885042887436622 ) ) ;
#4658=CARTESIAN_POINT ( 'NONE',  ( 0.000000000000000000, 0.000000000000000000, -25.03750572909317285 ) ) ;
#4662=CARTESIAN_POINT ( 'NONE',  ( -4.000000000000000000, 0.8576368993457507139, -3.433240632782198709 ) ) ;
#4667=AXIS2_PLACEMENT_3D ( 'NONE', #2552, #6507, #3915 ) ;
#4677=CARTESIAN_POINT ( 'NONE',  ( 1.243802165048773611, -3.900692638707475624, -3.223146290109810241 ) ) ;
#4692=VERTEX_POINT ( 'NONE', #2175 ) ;
#4695=FACE_OUTER_BOUND ( 'NONE', #498, .T. ) ;
#4699=CARTESIAN_POINT ( 'NONE',  ( -4.000000000000000000, -0.8232339106130515116, -3.430630286862743183 ) ) ;
#4708=AXIS2_PLACEMENT_3D ( 'NONE', #4648, #2489, #200 ) ;
#4710=CARTESIAN_POINT ( 'NONE',  ( 2.500000000000000888, 3.061616997868384127E-16, -4.974599999999998801 ) ) ;
#4712=EDGE_LOOP ( 'NONE', ( #5978, #55 ) ) ;
#4714=EDGE_CURVE ( 'NONE', #2565, #4184, #6600, .T. ) ;
#4717=CARTESIAN_POINT ( 'NONE',  ( 0.5469614295415388128, -4.303013824935362663, -3.535263753543555598 ) ) ;
#4727=CARTESIAN_POINT ( 'NONE',  ( 4.000000000000000000, -1.084202172485504434E-14, -3.142992957459231906 ) ) ;
#4729=CARTESIAN_POINT ( 'NONE',  ( -1.360585162435467455, 4.061296242128285883, -3.505054077164959203 ) ) ;
#4732=CARTESIAN_POINT ( 'NONE',  ( -2.344047193898593395, -3.265465875126480455, -1.054683074273691752E-14 ) ) ;
#4744=CIRCLE ( 'NONE', #2453, 5.384454397937118664 ) ;
#4747=ADVANCED_FACE ( 'NONE', ( #7083 ), #6590, .T. ) ;
#4755=CARTESIAN_POINT ( 'NONE',  ( -2.804994570502171047, -3.229033611042465335, -3.526374918436838701 ) ) ;
#4765=FACE_OUTER_BOUND ( 'NONE', #1021, .T. ) ;
#4767=ADVANCED_BREP_SHAPE_REPRESENTATION ( '', ( #5831, #1963 ), #4487 ) ;
#4772=CARTESIAN_POINT ( 'NONE',  ( -4.211405944401398038, -2.460460786169389902, -3.751298493805494072 ) ) ;
#4778=EDGE_LOOP ( 'NONE', ( #5629, #3995, #6125, #1253, #7257 ) ) ;
#4784=CARTESIAN_POINT ( 'NONE',  ( 1.567478505476134606E-15, 4.618802153517012066, -3.433295621305382905 ) ) ;
#4786=ORIENTED_EDGE ( 'NONE', *, *, #958, .T. ) ;
#4790=ORIENTED_EDGE ( 'NONE', *, *, #623, .T. ) ;
#4792=CARTESIAN_POINT ( 'NONE',  ( -0.5636800770129166693, -4.293361309317430319, -3.531542292955206275 ) ) ;
#4793=CARTESIAN_POINT ( 'NONE',  ( 4.101954839143060028, 2.368264730582927857, -3.681130640444267854 ) ) ;
#4797=CARTESIAN_POINT ( 'NONE',  ( 0.000000000000000000, 0.000000000000000000, -4.484454397937119197 ) ) ;
#4804=VECTOR ( 'NONE', #2610, 999.9999999999998863 ) ;
#4815=ORIENTED_EDGE ( 'NONE', *, *, #2889, .T. ) ;
#4835=CARTESIAN_POINT ( 'NONE',  ( 0.000000000000000000, 0.000000000000000000, 0.000000000000000000 ) ) ;
#4846=EDGE_CURVE ( 'NONE', #709, #4934, #5515, .T. ) ;
#4863=CARTESIAN_POINT ( 'NONE',  ( 4.000000000000000000, -2.309401076758514915, -3.433295621305383349 ) ) ;
#4864=ORIENTED_EDGE ( 'NONE', *, *, #5739, .F. ) ;
#4872=FACE_OUTER_BOUND ( 'NONE', #2810, .T. ) ;
#4876=CARTESIAN_POINT ( 'NONE',  ( 5.384454397937118664, 0.000000000000000000, -5.000000000000000000 ) ) ;
#4881=CARTESIAN_POINT ( 'NONE',  ( 4.211140560182196957, 2.431303136016536470, -3.745885042887433514 ) ) ;
#4904=B_SPLINE_CURVE_WITH_KNOTS ( 'NONE', 3,
 ( #1539, #3693, #5995, #6636, #6114, #3111, #2566, #2006 ),
 .UNSPECIFIED., .F., .F.,
 ( 4, 2, 2, 4 ),
 ( 0.000000000000000000, 0.002450665683189820997, 0.003675998524784731495, 0.004901331366379641993 ),
 .UNSPECIFIED. ) ;
#4905=ORIENTED_EDGE ( 'NONE', *, *, #3499, .T. ) ;
#4909=DIRECTION ( 'NONE',  ( -0.000000000000000000, -0.000000000000000000, 1.000000000000000000 ) ) ;
#4911=CARTESIAN_POINT ( 'NONE',  ( -4.000000000000000000, -2.309401076758512694, -5.000000000000000000 ) ) ;
#4921=CARTESIAN_POINT ( 'NONE',  ( 2.290893957444128645E-15, 4.647089433458768681, -3.572167766733382877 ) ) ;
#4925=EDGE_LOOP ( 'NONE', ( #3151, #7058, #6805 ) ) ;
#4932=EDGE_CURVE ( 'NONE', #6701, #2174, #792, .T. ) ;
#4934=VERTEX_POINT ( 'NONE', #2694 ) ;
#4936=CARTESIAN_POINT ( 'NONE',  ( 4.000000000000000000, -1.677850389431204459, -3.535268758346977513 ) ) ;
#4942=CARTESIAN_POINT ( 'NONE',  ( 1.999999999999998224, -3.464101615137772594, -3.142992957459239012 ) ) ;
#4947=CLOSED_SHELL ( 'NONE', ( #5264, #5250, #1326, #966, #2716, #2853, #5123, #3296, #2915, #5642, #6495, #301, #2261, #4058, #1993, #536, #608, #3105, #599, #6678, #4747, #6786, #487, #1751, #3946, #1272, #5479, #1610, #1852, #2770, #2035, #2255 ) ) ;
#4950=CARTESIAN_POINT ( 'NONE',  ( 3.999999999999999112, -0.7890432684750902093, -0.04868663549882291247 ) ) ;
#4951=CARTESIAN_POINT ( 'NONE',  ( 1.390230914382191596, 4.043987460488659202, -3.502507215260488582 ) ) ;
#4952=DIRECTION ( 'NONE',  ( 0.000000000000000000, 0.000000000000000000, -1.000000000000000000 ) ) ;
#4955=AXIS2_PLACEMENT_3D ( 'NONE', #3090, #6602, #5393 ) ;
#4986=PLANE ( 'NONE',  #3847 ) ;
#4998=CARTESIAN_POINT ( 'NONE',  ( -4.000000000000000000, 0.000000000000000000, 0.000000000000000000 ) ) ;
#5021=CARTESIAN_POINT ( 'NONE',  ( 0.3198814748697593746, 4.434118497892183264, -0.3507732604232499107 ) ) ;
#5023=SHAPE_REPRESENTATION ( 'hex flange nut gradea_iso_ISO - 4161 - M5 - N', ( #1963 ), #4487 ) ;
#5028=ORIENTED_EDGE ( 'NONE', *, *, #2154, .F. ) ;
#5035=PRODUCT_DEFINITION_CONTEXT ( 'detailed design', #3620, 'design' ) ;
#5041=CARTESIAN_POINT ( 'NONE',  ( -1.654252653721913102, -3.663718938583024443, -0.01223254789874440342 ) ) ;
#5045=B_SPLINE_CURVE_WITH_KNOTS ( 'NONE', 3,
 ( #693, #1795, #4086, #754, #168, #1836 ),
 .UNSPECIFIED., .F., .F.,
 ( 4, 2, 4 ),
 ( 0.002365888236227977302, 0.003551327329835078910, 0.004736766423442180518 ),
 .UNSPECIFIED. ) ;
#5068=CARTESIAN_POINT ( 'NONE',  ( -4.203833317240879275, -1.627343821129593859, -3.597273115243890818 ) ) ;
#5072=DIRECTION ( 'NONE',  ( 0.8660254037844374864, -0.5000000000000018874, 0.000000000000000000 ) ) ;
#5083=AXIS2_PLACEMENT_3D ( 'NONE', #2172, #1140, #1622 ) ;
#5088=ORIENTED_EDGE ( 'NONE', *, *, #6657, .T. ) ;
#5092=CIRCLE ( 'NONE', #2904, 2.100000000000000089 ) ;
#5094=EDGE_CURVE ( 'NONE', #5816, #76, #1482, .T. ) ;
#5096=VECTOR ( 'NONE', #4495, 1000.000000000000227 ) ;
#5099=DIRECTION ( 'NONE',  ( 1.000000000000000000, 0.000000000000000000, 0.000000000000000000 ) ) ;
#5123=ADVANCED_FACE ( 'NONE', ( #2243 ), #6830, .F. ) ;
#5132=CARTESIAN_POINT ( 'NONE',  ( 0.000000000000000000, 0.000000000000000000, 0.000000000000000000 ) ) ;
#5148=CARTESIAN_POINT ( 'NONE',  ( 0.02448733951239481094, 4.877042772274728044, -3.751161874094022242 ) ) ;
#5150=( NAMED_UNIT ( * ) SI_UNIT ( $, .STERADIAN. ) SOLID_ANGLE_UNIT ( ) );
#5154=ORIENTED_EDGE ( 'NONE', *, *, #184, .T. ) ;
#5164=CARTESIAN_POINT ( 'NONE',  ( -4.204015924366189871, 1.626724848190922446, -3.610627190413390419 ) ) ;
#5175=CARTESIAN_POINT ( 'NONE',  ( 4.198928548860774157, -0.8158838809860124996, -3.526471437616918170 ) ) ;
#5182=CIRCLE ( 'NONE', #1117, 4.000000000000000000 ) ;
#5183=CARTESIAN_POINT ( 'NONE',  ( -2.100000000000000089, 2.571758278209441957E-16, -4.694516984716113228 ) ) ;
#5184=EDGE_CURVE ( 'NONE', #2174, #2565, #7063, .T. ) ;
#5191=AXIS2_PLACEMENT_3D ( 'NONE', #6860, #1479, #2240 ) ;
#5211=CARTESIAN_POINT ( 'NONE',  ( -2.449848172108560540, -3.432307619358754724, -3.503702292528910078 ) ) ;
#5221=LINE ( 'NONE', #2254, #2408 ) ;
#5231=CARTESIAN_POINT ( 'NONE',  ( -2.687328764639638656, 3.067272167851286202, -0.05923475698270370959 ) ) ;
#5235=ORIENTED_EDGE ( 'NONE', *, *, #2783, .F. ) ;
#5236=CARTESIAN_POINT ( 'NONE',  ( -4.197393957002303999, -0.8151795401431414234, -3.503767560748935139 ) ) ;
#5238=FACE_BOUND ( 'NONE', #1155, .T. ) ;
#5242=CARTESIAN_POINT ( 'NONE',  ( 0.000000000000000000, 0.000000000000000000, -4.000000000000000000 ) ) ;
#5249=DIRECTION ( 'NONE',  ( -0.5000000000000016653, 0.8660254037844378194, 0.000000000000000000 ) ) ;
#5250=ADVANCED_FACE ( 'NONE', ( #2452 ), #2959, .F. ) ;
#5259=CARTESIAN_POINT ( 'NONE',  ( -4.204114297095464359, 1.660363174096617156, -3.602136431857887011 ) ) ;
#5262=EDGE_LOOP ( 'NONE', ( #1524, #5713, #6429 ) ) ;
#5263=FACE_OUTER_BOUND ( 'NONE', #4472, .T. ) ;
#5264=ADVANCED_FACE ( 'NONE', ( #6962 ), #2933, .F. ) ;
#5278=VERTEX_POINT ( 'NONE', #4040 ) ;
#5281=ORIENTED_EDGE ( 'NONE', *, *, #3338, .T. ) ;
#5283=CARTESIAN_POINT ( 'NONE',  ( 0.1750025118121568690, 4.719839900820621104, -3.469254087858248070 ) ) ;
#5288=ORIENTED_EDGE ( 'NONE', *, *, #1885, .F. ) ;
#5298=CARTESIAN_POINT ( 'NONE',  ( -4.000000000000000000, -2.512220745329312610, -3.469390707569719901 ) ) ;
#5301=ORIENTED_EDGE ( 'NONE', *, *, #4235, .F. ) ;
#5331=CARTESIAN_POINT ( 'NONE',  ( 4.211140560182196957, 2.431303136016536470, -3.745885042887433514 ) ) ;
#5334=CARTESIAN_POINT ( 'NONE',  ( -4.000000000000000000, 1.677772373332757194, -3.535253723897187506 ) ) ;
#5342=EDGE_LOOP ( 'NONE', ( #6534, #5281, #6103 ) ) ;
#5349=ORIENTED_EDGE ( 'NONE', *, *, #2956, .T. ) ;
#5356=CARTESIAN_POINT ( 'NONE',  ( 4.000000000000000000, 0.1981133338132474442, 2.382280164152719704E-17 ) ) ;
#5361=CARTESIAN_POINT ( 'NONE',  ( -5.560781378645575757, 6.809993116116508640E-16, -4.000000000000000000 ) ) ;
#5367=DIRECTION ( 'NONE',  ( 1.000000000000000000, 0.000000000000000000, 0.000000000000000000 ) ) ;
#5378=CARTESIAN_POINT ( 'NONE',  ( 0.5276280594147412240, -4.314175951381924889, -3.320322319201654881 ) ) ;
#5387=CARTESIAN_POINT ( 'NONE',  ( 3.999999999999999112, -0.3979232138631231819, -5.929230630780099908E-17 ) ) ;
#5389=CARTESIAN_POINT ( 'NONE',  ( 4.024499207728657879, 2.323545700935571556, -3.572172305156506411 ) ) ;
#5392=DIRECTION ( 'NONE',  ( -0.8660254037844377084, -0.5000000000000015543, 0.000000000000000000 ) ) ;
#5393=DIRECTION ( 'NONE',  ( -1.000000000000000000, 0.000000000000000000, 0.000000000000000000 ) ) ;
#5395=VECTOR ( 'NONE', #1135, 1000.000000000000000 ) ;
#5403=ORIENTED_EDGE ( 'NONE', *, *, #2379, .F. ) ;
#5404=ORIENTED_EDGE ( 'NONE', *, *, #3209, .T. ) ;
#5429=CARTESIAN_POINT ( 'NONE',  ( 2.000000000000005329, -3.464101615137751722, 0.000000000000000000 ) ) ;
#5432=CARTESIAN_POINT ( 'NONE',  ( 0.000000000000000000, 0.000000000000000000, -5.000000000000000000 ) ) ;
#5450=CARTESIAN_POINT ( 'NONE',  ( -4.000000000000000000, 2.309401076758498483, -3.433295621305379353 ) ) ;
#5459=CARTESIAN_POINT ( 'NONE',  ( 0.6666666666666658525, -4.233901974057276085, -3.300726591567086476 ) ) ;
#5463=CARTESIAN_POINT ( 'NONE',  ( 4.000000000000000000, 0.9868501483902631932, -0.09357334158579604100 ) ) ;
#5469=FACE_OUTER_BOUND ( 'NONE', #5342, .T. ) ;
#5479=ADVANCED_FACE ( 'NONE', ( #5529 ), #1708, .F. ) ;
#5496=DIRECTION ( 'NONE',  ( -0.8660254037844373753, 0.5000000000000021094, 0.000000000000000000 ) ) ;
#5506=FACE_OUTER_BOUND ( 'NONE', #2048, .T. ) ;
#5509=AXIS2_PLACEMENT_3D ( 'NONE', #5885, #6422, #2975 ) ;
#5515=B_SPLINE_CURVE_WITH_KNOTS ( 'NONE', 3,
 ( #2462, #5929, #4727, #6487, #1867 ),
 .UNSPECIFIED., .F., .F.,
 ( 4, 1, 4 ),
 ( 0.000000000000000000, 0.002309401076758505790, 0.004618802153517011580 ),
 .UNSPECIFIED. ) ;
#5525=CARTESIAN_POINT ( 'NONE',  ( -1.999999999999999556, 3.464101615137754830, -3.142992957459232795 ) ) ;
#5526=DIRECTION ( 'NONE',  ( -1.000000000000000000, 0.000000000000000000, 0.000000000000000000 ) ) ;
#5529=FACE_OUTER_BOUND ( 'NONE', #4778, .T. ) ;
#5543=VERTEX_POINT ( 'NONE', #3848 ) ;
#5546=CARTESIAN_POINT ( 'NONE',  ( 4.000000000000000000, 0.000000000000000000, 0.000000000000000000 ) ) ;
#5551=VECTOR ( 'NONE', #5820, 1000.000000000000000 ) ;
#5560=CARTESIAN_POINT ( 'NONE',  ( -2.500000000000000888, 0.000000000000000000, -4.974599999999998801 ) ) ;
#5561=CARTESIAN_POINT ( 'NONE',  ( -1.312671235360383548, -3.860931062424228788, -0.05923475698271369466 ) ) ;
#5568=VECTOR ( 'NONE', #188, 1000.000000000000000 ) ;
#5583=EDGE_CURVE ( 'NONE', #853, #1606, #5669, .T. ) ;
#5589=CARTESIAN_POINT ( 'NONE',  ( 2.345747346278113987, -3.264484291692503870, -0.01223254789874484924 ) ) ;
#5598=CARTESIAN_POINT ( 'NONE',  ( -1.144235203016679359, -3.958177651039096911, -0.09382832055446428676 ) ) ;
#5602=ORIENTED_EDGE ( 'NONE', *, *, #5583, .T. ) ;
#5613=DIRECTION ( 'NONE',  ( -0.000000000000000000, -0.000000000000000000, 1.000000000000000000 ) ) ;
#5617=FACE_OUTER_BOUND ( 'NONE', #1575, .T. ) ;
#5624=CARTESIAN_POINT ( 'NONE',  ( 4.000000000000000000, 2.309401076758497151, -3.433295621305379353 ) ) ;
#5629=ORIENTED_EDGE ( 'NONE', *, *, #4411, .T. ) ;
#5639=VERTEX_POINT ( 'NONE', #4242 ) ;
#5640=SHAPE_DEFINITION_REPRESENTATION ( #4412, #5023 ) ;
#5642=ADVANCED_FACE ( 'NONE', ( #5263 ), #6361, .F. ) ;
#5644=EDGE_CURVE ( 'NONE', #5278, #4072, #6764, .T. ) ;
#5645=CARTESIAN_POINT ( 'NONE',  ( 4.211140560182196957, -2.431303136016555122, -3.745885042887436622 ) ) ;
#5647=DIRECTION ( 'NONE',  ( -0.000000000000000000, -0.000000000000000000, 1.000000000000000000 ) ) ;
#5649=CARTESIAN_POINT ( 'NONE',  ( 4.000000000000000000, 2.512223110932545023, -3.469391141908803711 ) ) ;
#5651=DIRECTION ( 'NONE',  ( 0.000000000000000000, 0.000000000000000000, -1.000000000000000000 ) ) ;
#5663=EDGE_LOOP ( 'NONE', ( #4469, #2689, #2256, #34, #4790, #6803, #3912 ) ) ;
#5669=CIRCLE ( 'NONE', #1806, 2.500000000000000888 ) ;
#5674=CARTESIAN_POINT ( 'NONE',  ( 4.024499207728657879, -2.323545700935587988, -3.572172305156509964 ) ) ;
#5678=CIRCLE ( 'NONE', #2793, 2.100000000000000089 ) ;
#5689=CARTESIAN_POINT ( 'NONE',  ( 0.3461262719736147297, -4.658553426539303821, -3.671615880910379381 ) ) ;
#5702=ORIENTED_EDGE ( 'NONE', *, *, #5583, .F. ) ;
#5703=DIRECTION ( 'NONE',  ( -0.000000000000000000, 0.000000000000000000, -1.000000000000000000 ) ) ;
#5705=CARTESIAN_POINT ( 'NONE',  ( -5.384454397937118664, 6.702023979852544604E-16, -5.000000000000000000 ) ) ;
#5713=ORIENTED_EDGE ( 'NONE', *, *, #5184, .T. ) ;
#5727=EDGE_LOOP ( 'NONE', ( #5028, #6889, #6077, #6935 ) ) ;
#5739=EDGE_CURVE ( 'NONE', #4072, #1932, #5755, .T. ) ;
#5745=LINE ( 'NONE', #619, #3347 ) ;
#5755=CIRCLE ( 'NONE', #2158, 4.000000000000000000 ) ;
#5760=CARTESIAN_POINT ( 'NONE',  ( -2.171643655288372443, 3.365003104552320767, 2.541098841762897165E-18 ) ) ;
#5763=DIRECTION ( 'NONE',  ( 0.000000000000000000, 0.000000000000000000, -1.000000000000000000 ) ) ;
#5775=CARTESIAN_POINT ( 'NONE',  ( 4.207491450040567571, -2.029819825146485179, -3.671670828759567407 ) ) ;
#5780=CARTESIAN_POINT ( 'NONE',  ( 4.154306624731035846, -2.398490048085128556, -3.721999068284417955 ) ) ;
#5787=CIRCLE ( 'NONE', #6753, 5.384454397937118664 ) ;
#5809=CARTESIAN_POINT ( 'NONE',  ( -0.1404048886732797152, -4.699864953788083888, -3.686887068327043160 ) ) ;
#5816=VERTEX_POINT ( 'NONE', #4881 ) ;
#5820=DIRECTION ( 'NONE',  ( 0.000000000000000000, 0.000000000000000000, 1.000000000000000000 ) ) ;
#5829=DIRECTION ( 'NONE',  ( 1.000000000000000000, 0.000000000000000000, 0.000000000000000000 ) ) ;
#5831=MANIFOLD_SOLID_BREP ( 'EndChamfer', #4947 ) ;
#5832=CARTESIAN_POINT ( 'NONE',  ( -4.197477534772231955, 0.8522413273724368521, -3.505042416683225692 ) ) ;
#5837=CARTESIAN_POINT ( 'NONE',  ( 4.197393957002303999, 7.772902908466098641E-14, -3.503767560748929810 ) ) ;
#5838=CARTESIAN_POINT ( 'NONE',  ( 2.100000000000000089, 0.000000000000000000, -0.2800830152838844622 ) ) ;
#5854=DIRECTION ( 'NONE',  ( -0.000000000000000000, 0.000000000000000000, -1.000000000000000000 ) ) ;
#5862=DIRECTION ( 'NONE',  ( 0.000000000000000000, 0.000000000000000000, 1.000000000000000000 ) ) ;
#5877=B_SPLINE_CURVE_WITH_KNOTS ( 'NONE', 3,
 ( #2031, #930, #1529, #1565, #2717, #2680 ),
 .UNSPECIFIED., .F., .F.,
 ( 4, 2, 4 ),
 ( -3.640115492410698714E-06, 0.0002066546034006521879, 0.0004169493222937151081 ),
 .UNSPECIFIED. ) ;
#5878=PRESENTATION_STYLE_ASSIGNMENT (( #2937 ) ) ;
#5881=AXIS2_PLACEMENT_3D ( 'NONE', #2346, #6800, #18 ) ;
#5883=ORIENTED_EDGE ( 'NONE', *, *, #1808, .F. ) ;
#5885=CARTESIAN_POINT ( 'NONE',  ( 0.000000000000000000, 0.000000000000000000, 0.000000000000000000 ) ) ;
#5886=CARTESIAN_POINT ( 'NONE',  ( 0.1756481739660539498, -4.720212674038995360, -3.469390959564070620 ) ) ;
#5892=DIRECTION ( 'NONE',  ( -1.000000000000000000, 0.000000000000000000, 0.000000000000000000 ) ) ;
#5896=VECTOR ( 'NONE', #6131, 1000.000000000000227 ) ;
#5910=DIRECTION ( 'NONE',  ( 1.000000000000000000, 0.000000000000000000, 0.000000000000000000 ) ) ;
#5912=CONICAL_SURFACE ( 'NONE', #4708, 2.059999999999998721, 0.9599310885968738161 ) ;
#5929=CARTESIAN_POINT ( 'NONE',  ( 3.999999999999999112, -1.539600717839012978, -3.300726591567080703 ) ) ;
#5932=CARTESIAN_POINT ( 'NONE',  ( -4.000000000000000000, -2.309401076758515803, -0.4999999999999995559 ) ) ;
#5938=CARTESIAN_POINT ( 'NONE',  ( 1.391697335622810172, 4.043246145443375461, -3.503898532754365913 ) ) ;
#5949=CARTESIAN_POINT ( 'NONE',  ( -6.473970235329672780E-16, -4.862606272033106691, -3.745885042887442395 ) ) ;
#5950=VERTEX_POINT ( 'NONE', #5932 ) ;
#5963=ORIENTED_EDGE ( 'NONE', *, *, #7098, .T. ) ;
#5969=LINE ( 'NONE', #3550, #5551 ) ;
#5978=ORIENTED_EDGE ( 'NONE', *, *, #1284, .F. ) ;
#5983=CARTESIAN_POINT ( 'NONE',  ( -0.6666666666666651864, 4.233901974057260098, -3.300726591567081147 ) ) ;
#5988=CARTESIAN_POINT ( 'NONE',  ( 4.000000000000000000, -2.511475576507276042, -3.469253905236643565 ) ) ;
#5995=CARTESIAN_POINT ( 'NONE',  ( -2.805705207896067144, 3.226868319750155312, -3.503898532754364581 ) ) ;
#6006=EDGE_CURVE ( 'NONE', #807, #5543, #5678, .T. ) ;
#6031=EDGE_CURVE ( 'NONE', #4072, #5639, #5045, .T. ) ;
#6032=CARTESIAN_POINT ( 'NONE',  ( 4.000000000000000000, -2.471525695159793035, -3.686886880705770864 ) ) ;
#6066=CONICAL_SURFACE ( 'NONE', #2695, 2.500000000000000888, 0.9599310885968785900 ) ;
#6068=EDGE_CURVE ( 'NONE', #3899, #5639, #5969, .T. ) ;
#6073=CARTESIAN_POINT ( 'NONE',  ( 4.197478902586992966, -0.8524102783748346290, -3.505063281295504041 ) ) ;
#6075=DIRECTION ( 'NONE',  ( -1.000000000000000000, 0.000000000000000000, 0.000000000000000000 ) ) ;
#6077=ORIENTED_EDGE ( 'NONE', *, *, #1197, .T. ) ;
#6084=CARTESIAN_POINT ( 'NONE',  ( 3.355112389629172576, -2.681727112203168950, -0.2256878752776777242 ) ) ;
#6092=CARTESIAN_POINT ( 'NONE',  ( 2.344047193898588954, 3.265465875126468021, -5.031375706690542042E-16 ) ) ;
#6095=B_SPLINE_CURVE_WITH_KNOTS ( 'NONE', 3,
 ( #2466, #1835, #5389, #4793, #6530, #6489 ),
 .UNSPECIFIED., .F., .F.,
 ( 4, 2, 4 ),
 ( 0.000000000000000000, 0.0002095117440854730670, 0.0004190234881709461339 ),
 .UNSPECIFIED. ) ;
#6099=ORIENTED_EDGE ( 'NONE', *, *, #3591, .F. ) ;
#6101=EDGE_CURVE ( 'NONE', #3638, #5278, #4417, .T. ) ;
#6103=ORIENTED_EDGE ( 'NONE', *, *, #5644, .F. ) ;
#6106=FACE_OUTER_BOUND ( 'NONE', #5663, .T. ) ;
#6114=CARTESIAN_POINT ( 'NONE',  ( -1.393927851585477606, 4.043713361053528743, -3.526374918436835149 ) ) ;
#6119=CARTESIAN_POINT ( 'NONE',  ( -4.197393957002303999, -7.773935952363655451E-14, -3.503767560748929810 ) ) ;
#6120=CARTESIAN_POINT ( 'NONE',  ( 5.384454397937118664, 0.000000000000000000, -4.484454397937119197 ) ) ;
#6123=DIRECTION ( 'NONE',  ( -0.5000000000000019984, -0.8660254037844375974, 0.000000000000000000 ) ) ;
#6125=ORIENTED_EDGE ( 'NONE', *, *, #5094, .F. ) ;
#6129=DIRECTION ( 'NONE',  ( 1.000000000000000000, 0.000000000000000000, 0.000000000000000000 ) ) ;
#6131=DIRECTION ( 'NONE',  ( 0.9396926207859138680, 1.150791560227856926E-16, -0.3420201433256536139 ) ) ;
#6133=ORIENTED_EDGE ( 'NONE', *, *, #3648, .T. ) ;
#6146=CARTESIAN_POINT ( 'NONE',  ( -2.000000000000006661, 3.464101615137750834, 0.000000000000000000 ) ) ;
#6154=AXIS2_PLACEMENT_3D ( 'NONE', #4797, #1315, #760 ) ;
#6164=UNCERTAINTY_MEASURE_WITH_UNIT (LENGTH_MEASURE( 1.000000000000000082E-05 ), #1926, 'distance_accuracy_value', 'NONE');
#6173=PRODUCT_CONTEXT ( 'NONE', #3877, 'mechanical' ) ;
#6177=B_SPLINE_CURVE_WITH_KNOTS ( 'NONE', 3,
 ( #3632, #4732, #7088, #134, #3057, #1902 ),
 .UNSPECIFIED., .F., .F.,
 ( 4, 2, 4 ),
 ( 0.002365888236228001588, 0.003551327329835089319, 0.004736766423442177049 ),
 .UNSPECIFIED. ) ;
#6190=VECTOR ( 'NONE', #5862, 1000.000000000000000 ) ;
#6192=ORIENTED_EDGE ( 'NONE', *, *, #6882, .T. ) ;
#6198=CARTESIAN_POINT ( 'NONE',  ( 3.472371940585993855, 2.614027278893175321, -3.320322319201766792 ) ) ;
#6228=CARTESIAN_POINT ( 'NONE',  ( 0.6666666666666689611, 4.233901974057261874, -3.300726591567082480 ) ) ;
#6234=EDGE_CURVE ( 'NONE', #2174, #1932, #4601, .T. ) ;
#6250=CARTESIAN_POINT ( 'NONE',  ( 1.393927851585479161, -4.043713361053543842, -3.526374918436840922 ) ) ;
#6252=DIRECTION ( 'NONE',  ( 0.000000000000000000, 0.000000000000000000, 1.000000000000000000 ) ) ;
#6266=LINE ( 'NONE', #3363, #5395 ) ;
#6276=EDGE_CURVE ( 'NONE', #4634, #5950, #2767, .T. ) ;
#6277=CARTESIAN_POINT ( 'NONE',  ( 2.000000000000005329, -3.464101615137751722, 0.000000000000000000 ) ) ;
#6283=TOROIDAL_SURFACE ( 'NONE', #5083, 5.384454397937118664, 0.5155456020628804703 ) ;
#6304=AXIS2_PLACEMENT_3D ( 'NONE', #6963, #2934, #6311 ) ;
#6311=DIRECTION ( 'NONE',  ( -1.000000000000000000, 0.000000000000000000, 0.000000000000000000 ) ) ;
#6324=ORIENTED_EDGE ( 'NONE', *, *, #2889, .F. ) ;
#6329=DIRECTION ( 'NONE',  ( -0.000000000000000000, -0.000000000000000000, 1.000000000000000000 ) ) ;
#6330=EDGE_LOOP ( 'NONE', ( #4647, #2181, #624, #1594, #394 ) ) ;
#6331=CARTESIAN_POINT ( 'NONE',  ( -3.680118525130244400, 2.494084732383327285, -0.3507732604232449702 ) ) ;
#6338=DIRECTION ( 'NONE',  ( -1.000000000000000000, 0.000000000000000000, 0.000000000000000000 ) ) ;
#6340=CARTESIAN_POINT ( 'NONE',  ( 1.567478505476134606E-15, 4.618802153517012066, -3.433295621305382905 ) ) ;
#6345=CARTESIAN_POINT ( 'NONE',  ( 0.3208286057739604957, -4.433571671609698228, -0.3503314178412692548 ) ) ;
#6361=PLANE ( 'NONE',  #2771 ) ;
#6371=CARTESIAN_POINT ( 'NONE',  ( 1.257172072275274388, -3.892973519170983110, -3.433252694550781303 ) ) ;
#6374=( LENGTH_UNIT ( ) NAMED_UNIT ( * ) SI_UNIT ( .MILLI., .METRE. ) );
#6388=PRODUCT_DEFINITION_FORMATION_WITH_SPECIFIED_SOURCE ( 'ANY', '', #7153, .NOT_KNOWN. ) ;
#6397=CARTESIAN_POINT ( 'NONE',  ( -4.211399284164270895, 2.459729995988205964, -3.751162237960538715 ) ) ;
#6401=CARTESIAN_POINT ( 'NONE',  ( -2.000000000000006661, 3.464101615137750834, 0.000000000000000000 ) ) ;
#6407=CARTESIAN_POINT ( 'NONE',  ( 0.000000000000000000, 0.000000000000000000, -25.03750572909317285 ) ) ;
#6410=CARTESIAN_POINT ( 'NONE',  ( 4.141042297810615835, -2.227970268150433863, -3.687027686973623819 ) ) ;
#6413=FILL_AREA_STYLE_COLOUR ( '', #1144 ) ;
#6415=DIRECTION ( 'NONE',  ( 1.000000000000000000, 0.000000000000000000, 0.000000000000000000 ) ) ;
#6422=DIRECTION ( 'NONE',  ( 0.000000000000000000, 0.000000000000000000, -1.000000000000000000 ) ) ;
#6427=CARTESIAN_POINT ( 'NONE',  ( 1.567478505476134606E-15, 4.618802153517012066, -5.000000000000000000 ) ) ;
#6429=ORIENTED_EDGE ( 'NONE', *, *, #3569, .F. ) ;
#6447=CARTESIAN_POINT ( 'NONE',  ( -0.6920835326022555245, -4.454600218803899558, -3.597382984111586079 ) ) ;
#6448=ORIENTED_EDGE ( 'NONE', *, *, #1808, .T. ) ;
#6451=CARTESIAN_POINT ( 'NONE',  ( -3.453038570459499024, -2.625189405340453419, -3.535263753545272891 ) ) ;
#6462=ORIENTED_EDGE ( 'NONE', *, *, #5739, .T. ) ;
#6466=CARTESIAN_POINT ( 'NONE',  ( -4.000000000000000000, 2.511478553582031203, -3.469254451724764543 ) ) ;
#6467=UNCERTAINTY_MEASURE_WITH_UNIT (LENGTH_MEASURE( 1.000000000000000082E-05 ), #3830, 'distance_accuracy_value', 'NONE');
#6471=LINE ( 'NONE', #1226, #5568 ) ;
#6483=ORIENTED_EDGE ( 'NONE', *, *, #4163, .T. ) ;
#6487=CARTESIAN_POINT ( 'NONE',  ( 4.000000000000000888, 1.539600717838996990, -3.300726591567079815 ) ) ;
#6489=CARTESIAN_POINT ( 'NONE',  ( 4.211140560182196957, 2.431303136016536470, -3.745885042887433514 ) ) ;
#6495=ADVANCED_FACE ( 'NONE', ( #123 ), #2377, .T. ) ;
#6496=ORIENTED_EDGE ( 'NONE', *, *, #1263, .F. ) ;
#6507=DIRECTION ( 'NONE',  ( -0.000000000000000000, -0.000000000000000000, 1.000000000000000000 ) ) ;
#6510=ORIENTED_EDGE ( 'NONE', *, *, #3338, .F. ) ;
#6530=CARTESIAN_POINT ( 'NONE',  ( 4.154306624731137099, 2.398490048084935822, -3.721999068284414847 ) ) ;
#6534=ORIENTED_EDGE ( 'NONE', *, *, #6101, .F. ) ;
#6538=DIRECTION ( 'NONE',  ( -1.000000000000000000, 0.000000000000000000, 0.000000000000000000 ) ) ;
#6544=CARTESIAN_POINT ( 'NONE',  ( 1.312671235360372224, 3.860931062424219462, -0.05923475698270440348 ) ) ;
#6546=CARTESIAN_POINT ( 'NONE',  ( -4.211140560182196957, -2.431303136016552013, -3.745885042887436178 ) ) ;
#6552=DIRECTION ( 'NONE',  ( -1.000000000000000000, 0.000000000000000000, 0.000000000000000000 ) ) ;
#6565=CARTESIAN_POINT ( 'NONE',  ( -4.211140560182196957, 2.431303136016537803, -3.745885042887433514 ) ) ;
#6571=CARTESIAN_POINT ( 'NONE',  ( 2.804994570502171047, 3.229033611042449792, -3.526374918436834704 ) ) ;
#6576=ORIENTED_EDGE ( 'NONE', *, *, #3209, .F. ) ;
#6590=CONICAL_SURFACE ( 'NONE', #5509, 4.000000000000000000, 0.8911886515913786111 ) ;
#6592=EDGE_LOOP ( 'NONE', ( #2128, #220 ) ) ;
#6596=CARTESIAN_POINT ( 'NONE',  ( -2.742827927723112236, -3.035229711105190464, -3.433252694550595230 ) ) ;
#6600=B_SPLINE_CURVE_WITH_KNOTS ( 'NONE', 3,
 ( #6277, #2321, #4623, #3948, #6345, #1145 ),
 .UNSPECIFIED., .F., .F.,
 ( 4, 2, 4 ),
 ( 0.002365888236227967761, 0.003551327329835077609, 0.004736766423442186590 ),
 .UNSPECIFIED. ) ;
#6602=DIRECTION ( 'NONE',  ( 0.000000000000000000, 0.000000000000000000, -1.000000000000000000 ) ) ;
#6620=CARTESIAN_POINT ( 'NONE',  ( -4.101948962585905356, -2.368261337751088824, -3.681124513963624167 ) ) ;
#6636=CARTESIAN_POINT ( 'NONE',  ( -1.747541505913277282, 3.837784562140256650, -3.503702292528906526 ) ) ;
#6640=CARTESIAN_POINT ( 'NONE',  ( 4.000000000000000000, -1.942223658245635809, -0.3516579909967643691 ) ) ;
#6657=EDGE_CURVE ( 'NONE', #5543, #807, #5092, .T. ) ;
#6661=EDGE_LOOP ( 'NONE', ( #502, #486, #3680, #6496 ) ) ;
#6667=DIRECTION ( 'NONE',  ( -1.000000000000000000, 1.224646799147352714E-16, 0.000000000000000000 ) ) ;
#6678=ADVANCED_FACE ( 'NONE', ( #7226 ), #3271, .T. ) ;
#6684=CARTESIAN_POINT ( 'NONE',  ( 2.855764796983346177, -2.970025579236428737, -0.09382832055446485575 ) ) ;
#6685=CARTESIAN_POINT ( 'NONE',  ( 0.000000000000000000, 0.000000000000000000, 0.000000000000000000 ) ) ;
#6690=CARTESIAN_POINT ( 'NONE',  ( 2.000000000000008882, 3.464101615137749945, 0.000000000000000000 ) ) ;
#6691=CARTESIAN_POINT ( 'NONE',  ( -2.500000000000000888, 0.000000000000000000, -4.974599999999998801 ) ) ;
#6692=CARTESIAN_POINT ( 'NONE',  ( 2.000000000000008882, 3.464101615137749945, 0.000000000000000000 ) ) ;
#6695=DIRECTION ( 'NONE',  ( 0.000000000000000000, 0.000000000000000000, -1.000000000000000000 ) ) ;
#6701=VERTEX_POINT ( 'NONE', #7187 ) ;
#6708=DIRECTION ( 'NONE',  ( 0.000000000000000000, 0.000000000000000000, -1.000000000000000000 ) ) ;
#6717=FACE_OUTER_BOUND ( 'NONE', #4407, .T. ) ;
#6724=CARTESIAN_POINT ( 'NONE',  ( 2.000000000000005329, -3.464101615137751722, 0.000000000000000000 ) ) ;
#6728=CARTESIAN_POINT ( 'NONE',  ( -2.688821387764050996E-14, -4.618802153517012954, -0.4999999999999995559 ) ) ;
#6738=ORIENTED_EDGE ( 'NONE', *, *, #4078, .T. ) ;
#6743=LINE ( 'NONE', #1640, #7021 ) ;
#6747=DIRECTION ( 'NONE',  ( -1.000000000000000000, 0.000000000000000000, 0.000000000000000000 ) ) ;
#6753=AXIS2_PLACEMENT_3D ( 'NONE', #5432, #7054, #4165 ) ;
#6754=VECTOR ( 'NONE', #1120, 1000.000000000000000 ) ;
#6758=CARTESIAN_POINT ( 'NONE',  ( -0.1410422978106123659, 4.700232962125094893, -3.687027686973624707 ) ) ;
#6759=LINE ( 'NONE', #4427, #4804 ) ;
#6764=B_SPLINE_CURVE_WITH_KNOTS ( 'NONE', 3,
 ( #42, #6331, #705, #1225, #5231, #3710, #5760, #6401 ),
 .UNSPECIFIED., .F., .F.,
 ( 4, 2, 2, 4 ),
 ( 2.465131517071352357E-07, 0.001183067374689843057, 0.001774477805458910071, 0.002365888236227977302 ),
 .UNSPECIFIED. ) ;
#6767=EDGE_LOOP ( 'NONE', ( #749, #1745, #6886, #6099 ) ) ;
#6773=AXIS2_PLACEMENT_3D ( 'NONE', #297, #1960, #6667 ) ;
#6786=ADVANCED_FACE ( 'NONE', ( #1609 ), #2806, .T. ) ;
#6794=ORIENTED_EDGE ( 'NONE', *, *, #1002, .F. ) ;
#6800=DIRECTION ( 'NONE',  ( 0.000000000000000000, -0.000000000000000000, 1.000000000000000000 ) ) ;
#6803=ORIENTED_EDGE ( 'NONE', *, *, #2980, .T. ) ;
#6805=ORIENTED_EDGE ( 'NONE', *, *, #3316, .F. ) ;
#6810=B_SPLINE_CURVE_WITH_KNOTS ( 'NONE', 3,
 ( #7272, #5459, #4942, #978, #4863 ),
 .UNSPECIFIED., .F., .F.,
 ( 4, 1, 4 ),
 ( 5.640274452250024914E-20, 0.002309401076758505356, 0.004618802153517010713 ),
 .UNSPECIFIED. ) ;
#6821=CARTESIAN_POINT ( 'NONE',  ( 4.000000000000000000, 0.000000000000000000, 0.000000000000000000 ) ) ;
#6826=EDGE_LOOP ( 'NONE', ( #2703, #6738, #3355, #6794 ) ) ;
#6830=CYLINDRICAL_SURFACE ( 'NONE', #369, 2.100000000000000089 ) ;
#6844=STYLED_ITEM('',(#7446),#5831);
#6854=EDGE_LOOP ( 'NONE', ( #1958, #2042, #810, #7047 ) ) ;
#6860=CARTESIAN_POINT ( 'NONE',  ( 0.000000000000000000, 0.000000000000000000, -4.694516984716113228 ) ) ;
#6861=CONICAL_SURFACE ( 'NONE', #3606, 4.000000000000000000, 0.8911886515913786111 ) ;
#6874=B_SPLINE_CURVE_WITH_KNOTS ( 'NONE', 3,
 ( #3148, #5983, #5525, #4329, #5450 ),
 .UNSPECIFIED., .F., .F.,
 ( 4, 1, 4 ),
 ( 0.000000000000000000, 0.002309401076758506657, 0.004618802153517013315 ),
 .UNSPECIFIED. ) ;
#6882=EDGE_CURVE ( 'NONE', #1976, #431, #2197, .T. ) ;
#6886=ORIENTED_EDGE ( 'NONE', *, *, #7013, .T. ) ;
#6889=ORIENTED_EDGE ( 'NONE', *, *, #727, .F. ) ;
#6905=DIRECTION ( 'NONE',  ( 0.000000000000000000, 0.000000000000000000, -1.000000000000000000 ) ) ;
#6911=CARTESIAN_POINT ( 'NONE',  ( 4.197393957002303999, -0.4069871074557456780, -3.503767560748925813 ) ) ;
#6912=EDGE_CURVE ( 'NONE', #431, #1288, #1149, .T. ) ;
#6915=CARTESIAN_POINT ( 'NONE',  ( -1.257172072275743346, 3.892973519171203378, -3.433252694550776862 ) ) ;
#6922=LINE ( 'NONE', #4060, #6190 ) ;
#6935=ORIENTED_EDGE ( 'NONE', *, *, #6657, .F. ) ;
#6939=CARTESIAN_POINT ( 'NONE',  ( -4.141042297810615835, 2.227970268150415656, -3.687027686973619822 ) ) ;
#6944=ORIENTED_EDGE ( 'NONE', *, *, #4247, .F. ) ;
#6962=FACE_OUTER_BOUND ( 'NONE', #6826, .T. ) ;
#6963=CARTESIAN_POINT ( 'NONE',  ( 0.000000000000000000, 0.000000000000000000, -5.000000000000000888 ) ) ;
#7000=CIRCLE ( 'NONE', #73, 2.499999999999999556 ) ;
#7009=CARTESIAN_POINT ( 'NONE',  ( 1.360585162435110629, -4.061296242128317857, -3.505054077164905024 ) ) ;
#7013=EDGE_CURVE ( 'NONE', #4390, #7221, #7000, .T. ) ;
#7018=CARTESIAN_POINT ( 'NONE',  ( -4.175648173966055587, 2.207990556236529844, -3.469390959564062626 ) ) ;
#7019=CARTESIAN_POINT ( 'NONE',  ( -2.059999999999998721, 2.522772406243545965E-16, -0.3080913168122742518 ) ) ;
#7021=VECTOR ( 'NONE', #5, 1000.000000000000000 ) ;
#7029=FACE_OUTER_BOUND ( 'NONE', #798, .T. ) ;
#7040=CARTESIAN_POINT ( 'NONE',  ( -0.02448733951239248641, -4.877042772274742255, -3.751161874094027571 ) ) ;
#7047=ORIENTED_EDGE ( 'NONE', *, *, #2980, .F. ) ;
#7049=CARTESIAN_POINT ( 'NONE',  ( -4.175002511812151873, -2.208363329454905877, -3.469254087858246738 ) ) ;
#7052=EDGE_CURVE ( 'NONE', #4934, #3114, #6471, .T. ) ;
#7054=DIRECTION ( 'NONE',  ( -0.000000000000000000, -0.000000000000000000, 1.000000000000000000 ) ) ;
#7058=ORIENTED_EDGE ( 'NONE', *, *, #3499, .F. ) ;
#7061=CARTESIAN_POINT ( 'NONE',  ( 0.000000000000000000, 0.000000000000000000, -5.000000000000000000 ) ) ;
#7063=CIRCLE ( 'NONE', #3831, 4.000000000000000000 ) ;
#7073=CARTESIAN_POINT ( 'NONE',  ( 4.204115023516791005, -1.660442669500199919, -3.602151381774560068 ) ) ;
#7078=FACE_OUTER_BOUND ( 'NONE', #136, .T. ) ;
#7083=FACE_OUTER_BOUND ( 'NONE', #3369, .T. ) ;
#7084=CARTESIAN_POINT ( 'NONE',  ( 4.000000000000000000, 2.309401076758515803, -0.4999999999999995559 ) ) ;
#7085=CARTESIAN_POINT ( 'NONE',  ( -4.000000000000000000, -1.560351142792950618, -0.2242961665059814425 ) ) ;
#7088=CARTESIAN_POINT ( 'NONE',  ( -2.682243648011671588, -3.070208061305317759, -0.04852650426602272971 ) ) ;
#7095=CARTESIAN_POINT ( 'NONE',  ( 2.100000000000000089, 0.000000000000000000, -4.694516984716113228 ) ) ;
#7098=EDGE_CURVE ( 'NONE', #1949, #431, #557, .T. ) ;
#7105=CARTESIAN_POINT ( 'NONE',  ( 1.654252653721905331, 3.663718938583014229, -0.01223254789873410957 ) ) ;
#7122=CARTESIAN_POINT ( 'NONE',  ( -1.274258131565027874, -3.883108878240886241, -3.220599429844051009 ) ) ;
#7124=CARTESIAN_POINT ( 'NONE',  ( -4.000000000000000000, 0.7924765000094600165, -0.05906175389889745803 ) ) ;
#7137=DIRECTION ( 'NONE',  ( -0.000000000000000000, -0.000000000000000000, 1.000000000000000000 ) ) ;
#7151=ORIENTED_EDGE ( 'NONE', *, *, #623, .F. ) ;
#7153=PRODUCT ( 'hex flange nut gradea_iso_ISO - 4161 - M5 - N', 'hex flange nut gradea_iso_ISO - 4161 - M5 - N', '', ( #6173 ) ) ;
#7154=ORIENTED_EDGE ( 'NONE', *, *, #3426, .F. ) ;
#7170=DIRECTION ( 'NONE',  ( 1.000000000000000000, 0.000000000000000000, 0.000000000000000000 ) ) ;
#7173=AXIS2_PLACEMENT_3D ( 'NONE', #784, #4113, #3571 ) ;
#7187=CARTESIAN_POINT ( 'NONE',  ( 4.000000000000000000, -2.309401076758516691, -0.4999999999999995559 ) ) ;
#7197=DIRECTION ( 'NONE',  ( 1.000000000000000000, 0.000000000000000000, 0.000000000000000000 ) ) ;
#7207=CARTESIAN_POINT ( 'NONE',  ( 0.000000000000000000, 0.000000000000000000, 0.000000000000000000 ) ) ;
#7221=VERTEX_POINT ( 'NONE', #1528 ) ;
#7224=CARTESIAN_POINT ( 'NONE',  ( 4.000000000000000000, 1.680228229147133767, -3.316631783032546021 ) ) ;
#7225=DIRECTION ( 'NONE',  ( 0.000000000000000000, 0.000000000000000000, -1.000000000000000000 ) ) ;
#7226=FACE_OUTER_BOUND ( 'NONE', #5262, .T. ) ;
#7230=PLANE ( 'NONE',  #1462 ) ;
#7233=VERTEX_POINT ( 'NONE', #5949 ) ;
#7236=CARTESIAN_POINT ( 'NONE',  ( 0.5636800770130377947, 4.293361309317166530, -3.531542292954102713 ) ) ;
#7240=CARTESIAN_POINT ( 'NONE',  ( -4.000000000000000000, 1.941961291383472732, -0.3515519931180205448 ) ) ;
#7249=EDGE_CURVE ( 'NONE', #1000, #4634, #2083, .T. ) ;
#7257=ORIENTED_EDGE ( 'NONE', *, *, #4846, .F. ) ;
#7267=DIRECTION ( 'NONE',  ( 1.000000000000000000, 0.000000000000000000, 0.000000000000000000 ) ) ;
#7271=ORIENTED_EDGE ( 'NONE', *, *, #1885, .T. ) ;
#7272=CARTESIAN_POINT ( 'NONE',  ( -6.259644161404860030E-16, -4.618802153517027165, -3.433295621305388234 ) ) ;
#7288=CARTESIAN_POINT ( 'NONE',  ( 1.828356344711641102, 3.563200125723180900, -5.433716356636336675E-16 ) ) ;
#7292=FACE_OUTER_BOUND ( 'NONE', #4925, .T. ) ;
#7299=CARTESIAN_POINT ( 'NONE',  ( -2.500000000000000444, 3.061616997868383634E-16, -5.000000000000000888 ) ) ;
#7304=CARTESIAN_POINT ( 'NONE',  ( 0.000000000000000000, 0.000000000000000000, 0.000000000000000000 ) ) ;
#7317=B_SPLINE_CURVE_WITH_KNOTS ( 'NONE', 3,
 ( #2952, #144, #182, #2364, #2398 ),
 .UNSPECIFIED., .F., .F.,
 ( 4, 1, 4 ),
 ( 0.000000000000000000, 0.002309401076758505356, 0.004618802153517010713 ),
 .UNSPECIFIED. ) ;
#7321=EDGE_LOOP ( 'NONE', ( #663, #1659, #4323, #5702 ) ) ;
#7323=FACE_OUTER_BOUND ( 'NONE', #6854, .T. ) ;
#7324=B_SPLINE_CURVE_WITH_KNOTS ( 'NONE', 3,
 ( #2722, #5021, #4453, #2177, #6544, #7105, #7288, #6692 ),
 .UNSPECIFIED., .F., .F.,
 ( 4, 2, 2, 4 ),
 ( 2.465131517075058656E-07, 0.001183067374689851080, 0.001774477805458923299, 0.002365888236227995517 ),
 .UNSPECIFIED. ) ;
#7440=COLOUR_RGB('Black',0.12,0.14,0.17);
#7441=FILL_AREA_STYLE_COLOUR('',#7440);
#7442=FILL_AREA_STYLE('',(#7441));
#7443=SURFACE_STYLE_FILL_AREA(#7442);
#7444=SURFACE_SIDE_STYLE('',(#7443));
#7445=SURFACE_STYLE_USAGE(.BOTH.,#7444);
#7446=PRESENTATION_STYLE_ASSIGNMENT((#7445));
ENDSEC;
END-ISO-10303-21;
